ISO-10303-21;
HEADER;
FILE_DESCRIPTION (('STEP AP214'),
    '1' );
FILE_NAME ('hex nut gradec_iso_ISO - 4034 - M5 - N.step',
    '2026-10-03T12:29:21',
    ( '' ),
    ( '' ),
    'SwSTEP 2.0',
    'SolidWorks 2026',
    '' );
FILE_SCHEMA (( 'AUTOMOTIVE_DESIGN' ));
ENDSEC;

DATA;
#9=ORIENTED_EDGE ( 'NONE', *, *, #5715, .F. ) ;
#56=DIRECTION ( 'NONE',  ( 0.000000000000000000, 0.000000000000000000, 1.000000000000000000 ) ) ;
#97=B_SPLINE_CURVE_WITH_KNOTS ( 'NONE', 3,
 ( #16276, #17575, #14698, #9503, #6729, #17780 ),
 .UNSPECIFIED., .F., .F.,
 ( 4, 2, 4 ),
 ( 0.002336974151641604130, 0.003500975885716476211, 0.004664977619791348291 ),
 .UNSPECIFIED. ) ;
#102=FACE_OUTER_BOUND ( 'NONE', #4035, .T. ) ;
#143=CARTESIAN_POINT ( 'NONE',  ( 0.000000000000000000, 0.000000000000000000, 3.469446951953614189E-15 ) ) ;
#157=EDGE_LOOP ( 'NONE', ( #10780, #10369, #19381, #16296 ) ) ;
#167=ADVANCED_FACE ( 'NONE', ( #20203 ), #3671, .T. ) ;
#185=DIRECTION ( 'NONE',  ( 1.000000000000000000, 0.000000000000000000, 0.000000000000000000 ) ) ;
#201=ORIENTED_EDGE ( 'NONE', *, *, #18377, .T. ) ;
#204=CIRCLE ( 'NONE', #9346, 4.000000000000000888 ) ;
#225=AXIS2_PLACEMENT_3D ( 'NONE', #9690, #19631, #5323 ) ;
#232=VERTEX_POINT ( 'NONE', #20093 ) ;
#237=CONICAL_SURFACE ( 'NONE', #4643, 2.500000000000002220, 0.9599310885968777018 ) ;
#316=APPLICATION_CONTEXT ( 'automotive_design' ) ;
#319=CARTESIAN_POINT ( 'NONE',  ( 2.099999999999999645, 0.000000000000000000, -5.599999999999999645 ) ) ;
#379=CARTESIAN_POINT ( 'NONE',  ( 2.000000000000027089, 3.464101615137739731, -5.600000000000000533 ) ) ;
#422=AXIS2_PLACEMENT_3D ( 'NONE', #16823, #3876, #10248 ) ;
#465=ORIENTED_EDGE ( 'NONE', *, *, #10809, .T. ) ;
#481=CARTESIAN_POINT ( 'NONE',  ( -3.673643420401911275, -2.497823135841290565, -5.351519936624989704 ) ) ;
#520=VERTEX_POINT ( 'NONE', #20918 ) ;
#526=UNCERTAINTY_MEASURE_WITH_UNIT (LENGTH_MEASURE( 1.000000000000000082E-05 ), #19696, 'distance_accuracy_value', 'NONE');
#542=ORIENTED_EDGE ( 'NONE', *, *, #11407, .F. ) ;
#566=ORIENTED_EDGE ( 'NONE', *, *, #15947, .T. ) ;
#619=ORIENTED_EDGE ( 'NONE', *, *, #11741, .F. ) ;
#628=DIRECTION ( 'NONE',  ( -0.000000000000000000, -0.000000000000000000, 1.000000000000000000 ) ) ;
#636=DIRECTION ( 'NONE',  ( -1.000000000000000000, 0.000000000000000000, 0.000000000000000000 ) ) ;
#663=CARTESIAN_POINT ( 'NONE',  ( 1.155036213957052500E-14, 4.618802153517020059, -5.599999999999999645 ) ) ;
#679=CARTESIAN_POINT ( 'NONE',  ( 0.000000000000000000, 0.000000000000000000, 0.000000000000000000 ) ) ;
#694=VECTOR ( 'NONE', #20480, 1000.000000000000000 ) ;
#701=VERTEX_POINT ( 'NONE', #8605 ) ;
#711=B_SPLINE_CURVE_WITH_KNOTS ( 'NONE', 3,
 ( #7231, #5536, #12223, #13714, #18693, #3841 ),
 .UNSPECIFIED., .F., .F.,
 ( 4, 2, 4 ),
 ( 0.006456566858647394894, 0.007625406818786665576, 0.008794246778925936259 ),
 .UNSPECIFIED. ) ;
#735=CONICAL_SURFACE ( 'NONE', #11896, 4.000000000000000000, 1.047197551196595855 ) ;
#750=DIRECTION ( 'NONE',  ( -1.000000000000000000, 0.000000000000000000, 0.000000000000000000 ) ) ;
#760=DIRECTION ( 'NONE',  ( -0.000000000000000000, -0.000000000000000000, 1.000000000000000000 ) ) ;
#789=FILL_AREA_STYLE_COLOUR ( '', #16102 ) ;
#790=DIRECTION ( 'NONE',  ( -1.000000000000000000, 0.000000000000000000, 0.000000000000000000 ) ) ;
#869=DIRECTION ( 'NONE',  ( 1.000000000000000000, 0.000000000000000000, 0.000000000000000000 ) ) ;
#871=EDGE_LOOP ( 'NONE', ( #2334, #11167, #13816, #14112, #20707, #13085 ) ) ;
#926=CARTESIAN_POINT ( 'NONE',  ( -4.000000000000000000, -2.309401076758531346, -5.242734410091827613 ) ) ;
#949=ADVANCED_FACE ( 'NONE', ( #1200 ), #13942, .T. ) ;
#964=VERTEX_POINT ( 'NONE', #3390 ) ;
#988=VERTEX_POINT ( 'NONE', #19106 ) ;
#1026=EDGE_LOOP ( 'NONE', ( #11463, #10567, #20896 ) ) ;
#1048=CONICAL_SURFACE ( 'NONE', #2397, 4.000000000000000000, 1.047197551196595855 ) ;
#1051=SURFACE_STYLE_FILL_AREA ( #4103 ) ;
#1054=AXIS2_PLACEMENT_3D ( 'NONE', #7104, #2567, #13695 ) ;
#1055=CARTESIAN_POINT ( 'NONE',  ( 4.000000000000003553, 2.309401076758524685, -0.3572655899081733644 ) ) ;
#1077=EDGE_CURVE ( 'NONE', #1492, #12057, #9450, .T. ) ;
#1080=B_SPLINE_CURVE_WITH_KNOTS ( 'NONE', 3,
 ( #19450, #9709, #11496, #19760 ),
 .UNSPECIFIED., .F., .F.,
 ( 4, 4 ),
 ( 2.380737582495642427E-07, 0.002336974151641604130 ),
 .UNSPECIFIED. ) ;
#1167=AXIS2_PLACEMENT_3D ( 'NONE', #15816, #15501, #12651 ) ;
#1173=EDGE_CURVE ( 'NONE', #2494, #7434, #1775, .T. ) ;
#1200=FACE_OUTER_BOUND ( 'NONE', #19189, .T. ) ;
#1204=CARTESIAN_POINT ( 'NONE',  ( 0.000000000000000000, 0.000000000000000000, 0.000000000000000000 ) ) ;
#1225=ADVANCED_FACE ( 'NONE', ( #8466, #5493 ), #3798, .F. ) ;
#1260=ORIENTED_EDGE ( 'NONE', *, *, #1340, .F. ) ;
#1320=VERTEX_POINT ( 'NONE', #20123 ) ;
#1340=EDGE_CURVE ( 'NONE', #7434, #17615, #18406, .T. ) ;
#1347=AXIS2_PLACEMENT_3D ( 'NONE', #17925, #4887, #11354 ) ;
#1363=LINE ( 'NONE', #9504, #8717 ) ;
#1492=VERTEX_POINT ( 'NONE', #17905 ) ;
#1558=EDGE_LOOP ( 'NONE', ( #5571, #10917, #2045 ) ) ;
#1567=DIRECTION ( 'NONE',  ( 0.000000000000000000, -0.000000000000000000, 1.000000000000000000 ) ) ;
#1590=CONICAL_SURFACE ( 'NONE', #1904, 2.500000000000002220, 0.9599310885968777018 ) ;
#1634=CARTESIAN_POINT ( 'NONE',  ( 2.681483223904247648, -3.070647092368467224, -5.599999999999980105 ) ) ;
#1689=B_SPLINE_CURVE_WITH_KNOTS ( 'NONE', 3,
 ( #379, #3866, #2076, #8848, #6943, #13431 ),
 .UNSPECIFIED., .F., .F.,
 ( 4, 2, 4 ),
 ( 0.002336974151641576809, 0.003500975885716453226, 0.004664977619791330077 ),
 .UNSPECIFIED. ) ;
#1726=DIRECTION ( 'NONE',  ( -1.000000000000000000, 0.000000000000000000, 0.000000000000000000 ) ) ;
#1775=CIRCLE ( 'NONE', #19362, 4.000000000000000888 ) ;
#1792=FACE_OUTER_BOUND ( 'NONE', #3371, .T. ) ;
#1798=VECTOR ( 'NONE', #56, 1000.000000000000000 ) ;
#1808=CARTESIAN_POINT ( 'NONE',  ( 4.000000000000003553, -0.3902508023145564442, -1.995609623731131599E-15 ) ) ;
#1821=CARTESIAN_POINT ( 'NONE',  ( 4.000000000000003553, 2.309401076758480720, -5.599999999999999645 ) ) ;
#1829=CARTESIAN_POINT ( 'NONE',  ( 3.345653888883671101, -2.687187980154741140, -0.1391502195351564664 ) ) ;
#1883=AXIS2_PLACEMENT_3D ( 'NONE', #7227, #13709, #20157 ) ;
#1904=AXIS2_PLACEMENT_3D ( 'NONE', #6518, #3652, #11608 ) ;
#1931=ORIENTED_EDGE ( 'NONE', *, *, #18504, .T. ) ;
#1948=EDGE_LOOP ( 'NONE', ( #19534, #18929, #17186, #3457, #542, #6703 ) ) ;
#1952=EDGE_CURVE ( 'NONE', #17356, #12057, #20748, .T. ) ;
#1954=AXIS2_PLACEMENT_3D ( 'NONE', #11006, #17482, #10903 ) ;
#2020=ORIENTED_EDGE ( 'NONE', *, *, #12147, .T. ) ;
#2025=CARTESIAN_POINT ( 'NONE',  ( 3.999999999999990674, -2.309401076758548221, -5.242734410091827613 ) ) ;
#2030=CARTESIAN_POINT ( 'NONE',  ( 4.000000000000000000, 0.000000000000000000, 0.000000000000000000 ) ) ;
#2044=DIRECTION ( 'NONE',  ( -0.000000000000000000, -0.000000000000000000, 1.000000000000000000 ) ) ;
#2045=ORIENTED_EDGE ( 'NONE', *, *, #14974, .T. ) ;
#2076=CARTESIAN_POINT ( 'NONE',  ( 2.678494666091051801, 3.072372537026355044, -5.565789719053469753 ) ) ;
#2084=EDGE_CURVE ( 'NONE', #15954, #13448, #5637, .T. ) ;
#2117=AXIS2_PLACEMENT_3D ( 'NONE', #19356, #4841, #20632 ) ;
#2119=CARTESIAN_POINT ( 'NONE',  ( 1.660531772554325158, -3.660093687634888404, -5.599999999999981881 ) ) ;
#2205=EDGE_CURVE ( 'NONE', #520, #6509, #13499, .T. ) ;
#2213=UNCERTAINTY_MEASURE_WITH_UNIT (LENGTH_MEASURE( 1.000000000000000082E-05 ), #2484, 'distance_accuracy_value', 'NONE');
#2223=CARTESIAN_POINT ( 'NONE',  ( 0.000000000000000000, 0.000000000000000000, 0.000000000000000000 ) ) ;
#2243=VECTOR ( 'NONE', #19192, 1000.000000000000000 ) ;
#2263=CIRCLE ( 'NONE', #9361, 4.000000000000000888 ) ;
#2332=EDGE_CURVE ( 'NONE', #20245, #15954, #19753, .T. ) ;
#2334=ORIENTED_EDGE ( 'NONE', *, *, #20490, .T. ) ;
#2344=SHAPE_REPRESENTATION ( 'hex nut gradec_iso_ISO - 4034 - M5 - N', ( #12461 ), #12750 ) ;
#2364=PLANE ( 'NONE',  #1883 ) ;
#2368=CARTESIAN_POINT ( 'NONE',  ( -4.000000000000000000, -0.7779732554280792689, -0.03354435108167819896 ) ) ;
#2397=AXIS2_PLACEMENT_3D ( 'NONE', #679, #16899, #790 ) ;
#2428=CARTESIAN_POINT ( 'NONE',  ( 0.6554360035617794455, -4.240386000424091861, -0.1586754815285204845 ) ) ;
#2471=ADVANCED_FACE ( 'NONE', ( #6682 ), #14640, .F. ) ;
#2484=( LENGTH_UNIT ( ) NAMED_UNIT ( * ) SI_UNIT ( .MILLI., .METRE. ) );
#2492=DIRECTION ( 'NONE',  ( 1.000000000000000000, 0.000000000000000000, 0.000000000000000000 ) ) ;
#2494=VERTEX_POINT ( 'NONE', #18028 ) ;
#2496=EDGE_CURVE ( 'NONE', #19685, #17353, #4136, .T. ) ;
#2567=DIRECTION ( 'NONE',  ( 0.000000000000000000, -0.000000000000000000, 1.000000000000000000 ) ) ;
#2572=ORIENTED_EDGE ( 'NONE', *, *, #20490, .F. ) ;
#2599=B_SPLINE_CURVE_WITH_KNOTS ( 'NONE', 3,
 ( #10966, #4713, #10768, #12558 ),
 .UNSPECIFIED., .F., .F.,
 ( 4, 4 ),
 ( 2.380737581618737539E-07, 0.002336974151641576809 ),
 .UNSPECIFIED. ) ;
#2629=CARTESIAN_POINT ( 'NONE',  ( 0.3263565795980685191, -4.430380094434308802, -5.351519936624961282 ) ) ;
#2641=ORIENTED_EDGE ( 'NONE', *, *, #11407, .T. ) ;
#2661=DIRECTION ( 'NONE',  ( 0.000000000000000000, -0.000000000000000000, 1.000000000000000000 ) ) ;
#2721=DIRECTION ( 'NONE',  ( -0.000000000000000000, -0.000000000000000000, 1.000000000000000000 ) ) ;
#2748=CARTESIAN_POINT ( 'NONE',  ( 1.321505333908968627, -3.855830693249186147, -0.03421028094655685636 ) ) ;
#2765=EDGE_CURVE ( 'NONE', #8003, #8586, #13958, .T. ) ;
#2773=ORIENTED_EDGE ( 'NONE', *, *, #15336, .T. ) ;
#2789=AXIS2_PLACEMENT_3D ( 'NONE', #20333, #4238, #12405 ) ;
#2791=DIRECTION ( 'NONE',  ( -1.000000000000000000, 0.000000000000000000, 0.000000000000000000 ) ) ;
#2820=CARTESIAN_POINT ( 'NONE',  ( -4.000000000000000000, -1.549102112939103826, -5.442104661404060906 ) ) ;
#2834=FACE_OUTER_BOUND ( 'NONE', #14790, .T. ) ;
#2846=AXIS2_PLACEMENT_3D ( 'NONE', #18057, #19325, #16558 ) ;
#2851=CIRCLE ( 'NONE', #3523, 2.099999999999999645 ) ;
#2885=EDGE_LOOP ( 'NONE', ( #3168, #14036, #4906, #619 ) ) ;
#2892=EDGE_CURVE ( 'NONE', #8586, #964, #11913, .T. ) ;
#2921=AXIS2_PLACEMENT_3D ( 'NONE', #8178, #14961, #14646 ) ;
#2987=CARTESIAN_POINT ( 'NONE',  ( 2.500000000000002220, 3.061616997868386099E-16, -5.574599999999999334 ) ) ;
#3006=ADVANCED_FACE ( 'NONE', ( #1792 ), #7834, .T. ) ;
#3015=ORIENTED_EDGE ( 'NONE', *, *, #6009, .T. ) ;
#3149=CARTESIAN_POINT ( 'NONE',  ( 1.318516776095788545, 3.857556137907071747, -5.600000000000003197 ) ) ;
#3168=ORIENTED_EDGE ( 'NONE', *, *, #1952, .T. ) ;
#3201=DIRECTION ( 'NONE',  ( 0.000000000000000000, 0.000000000000000000, 1.000000000000000000 ) ) ;
#3211=CARTESIAN_POINT ( 'NONE',  ( 4.000000000000003553, 2.309401076758524685, -0.3572655899081733644 ) ) ;
#3292=ADVANCED_FACE ( 'NONE', ( #15969 ), #14190, .F. ) ;
#3317=CARTESIAN_POINT ( 'NONE',  ( 2.681483223904246760, -3.070647092368467668, -2.072929885643508434E-14 ) ) ;
#3361=DIRECTION ( 'NONE',  ( 0.000000000000000000, 0.000000000000000000, 1.000000000000000000 ) ) ;
#3371=EDGE_LOOP ( 'NONE', ( #12735, #6952, #566, #12322, #14100, #14129 ) ) ;
#3390=CARTESIAN_POINT ( 'NONE',  ( -2.000000000000022649, -3.464101615137742396, -5.600000000000000533 ) ) ;
#3391=AXIS2_PLACEMENT_3D ( 'NONE', #4599, #6391, #12777 ) ;
#3411=FACE_OUTER_BOUND ( 'NONE', #871, .T. ) ;
#3457=ORIENTED_EDGE ( 'NONE', *, *, #16497, .F. ) ;
#3475=CARTESIAN_POINT ( 'NONE',  ( 0.000000000000000000, 0.000000000000000000, -5.600000000000000533 ) ) ;
#3489=CARTESIAN_POINT ( 'NONE',  ( 1.214306433183764966E-14, 4.618802153517020059, 0.000000000000000000 ) ) ;
#3507=CARTESIAN_POINT ( 'NONE',  ( 3.999999999999990674, -2.309401076758548221, -5.242734410091827613 ) ) ;
#3523=AXIS2_PLACEMENT_3D ( 'NONE', #10846, #7984, #9364 ) ;
#3570=ORIENTED_EDGE ( 'NONE', *, *, #18438, .F. ) ;
#3582=COLOUR_RGB ( '', 0.09019608, 0.27058824, 0.51372549) ;
#3652=DIRECTION ( 'NONE',  ( 0.000000000000000000, 0.000000000000000000, -1.000000000000000000 ) ) ;
#3671=PLANE ( 'NONE',  #422 ) ;
#3695=CARTESIAN_POINT ( 'NONE',  ( 2.000000000000010658, -3.464101615137748169, -5.600000000000000533 ) ) ;
#3715=CARTESIAN_POINT ( 'NONE',  ( 4.000000000000003553, 0.3904826640788068293, -5.599999999999999645 ) ) ;
#3716=CARTESIAN_POINT ( 'NONE',  ( -4.000000000000000000, -1.549102112939103826, -0.1578953385959410982 ) ) ;
#3741=ADVANCED_FACE ( 'NONE', ( #12608 ), #15885, .F. ) ;
#3761=DIRECTION ( 'NONE',  ( -1.000000000000000000, 0.000000000000000000, 0.000000000000000000 ) ) ;
#3762=CONICAL_SURFACE ( 'NONE', #5460, 4.000000000000000000, 1.047197551196595855 ) ;
#3786=SURFACE_SIDE_STYLE ('',( #1051 ) ) ;
#3794=EDGE_CURVE ( 'NONE', #9645, #14918, #4656, .T. ) ;
#3798=PLANE ( 'NONE',  #7870 ) ;
#3807=ORIENTED_EDGE ( 'NONE', *, *, #5704, .F. ) ;
#3841=CARTESIAN_POINT ( 'NONE',  ( -4.000000000000000000, 2.309401076758531346, -5.242734410091827613 ) ) ;
#3843=CONICAL_SURFACE ( 'NONE', #2846, 2.060000000000000941, 0.9599310885968777018 ) ;
#3862=FACE_OUTER_BOUND ( 'NONE', #13317, .T. ) ;
#3866=CARTESIAN_POINT ( 'NONE',  ( 2.339468227445713921, 3.268109542640642573, -5.600000000000002309 ) ) ;
#3876=DIRECTION ( 'NONE',  ( 0.5000000000000025535, -0.8660254037844371533, 0.000000000000000000 ) ) ;
#3968=CARTESIAN_POINT ( 'NONE',  ( 0.000000000000000000, 0.000000000000000000, 0.000000000000000000 ) ) ;
#3980=DIRECTION ( 'NONE',  ( -0.000000000000000000, -0.000000000000000000, 1.000000000000000000 ) ) ;
#3988=CARTESIAN_POINT ( 'NONE',  ( -0.3263565795980851170, 4.430380094434251959, -5.351519936624993257 ) ) ;
#4030=DIRECTION ( 'NONE',  ( 1.000000000000000000, 0.000000000000000000, 0.000000000000000000 ) ) ;
#4035=EDGE_LOOP ( 'NONE', ( #4943, #19374, #15478 ) ) ;
#4103=FILL_AREA_STYLE ('',( #15241 ) ) ;
#4121=DIRECTION ( 'NONE',  ( -1.000000000000000000, 8.881784197001252323E-16, 0.000000000000000000 ) ) ;
#4136=B_SPLINE_CURVE_WITH_KNOTS ( 'NONE', 3,
 ( #8171, #19611, #7975, #12955 ),
 .UNSPECIFIED., .F., .F.,
 ( 4, 4 ),
 ( 2.380737581620991176E-07, 0.002336974151641539946 ),
 .UNSPECIFIED. ) ;
#4188=EDGE_CURVE ( 'NONE', #4388, #19414, #11152, .T. ) ;
#4191=AXIS2_PLACEMENT_3D ( 'NONE', #1821, #11464, #3201 ) ;
#4198=AXIS2_PLACEMENT_3D ( 'NONE', #15124, #3980, #3761 ) ;
#4206=CARTESIAN_POINT ( 'NONE',  ( 1.321505333908969293, -3.855830693249186147, -5.565789719053443996 ) ) ;
#4234=CARTESIAN_POINT ( 'NONE',  ( 1.660531772554323604, -3.660093687634888848, -2.106514470958295182E-14 ) ) ;
#4238=DIRECTION ( 'NONE',  ( 0.000000000000000000, -0.000000000000000000, 1.000000000000000000 ) ) ;
#4248=CIRCLE ( 'NONE', #7278, 2.500000000000002220 ) ;
#4304=B_SPLINE_CURVE_WITH_KNOTS ( 'NONE', 3,
 ( #12665, #20493, #19125, #14246, #20597, #9372 ),
 .UNSPECIFIED., .F., .F.,
 ( 4, 2, 4 ),
 ( 0.002336974151641539946, 0.003500975885716448889, 0.004664977619791357832 ),
 .UNSPECIFIED. ) ;
#4355=CARTESIAN_POINT ( 'NONE',  ( 4.000000000000003553, 2.309401076758480720, -5.599999999999999645 ) ) ;
#4373=DIRECTION ( 'NONE',  ( 0.000000000000000000, 0.000000000000000000, 1.000000000000000000 ) ) ;
#4388=VERTEX_POINT ( 'NONE', #6781 ) ;
#4423=ORIENTED_EDGE ( 'NONE', *, *, #19718, .F. ) ;
#4429=CARTESIAN_POINT ( 'NONE',  ( -4.000000000000000000, 0.000000000000000000, -5.599999999999999645 ) ) ;
#4443=DIRECTION ( 'NONE',  ( 0.000000000000000000, 0.000000000000000000, -1.000000000000000000 ) ) ;
#4502=EDGE_LOOP ( 'NONE', ( #8785, #12717, #8454, #3807 ) ) ;
#4507=CARTESIAN_POINT ( 'NONE',  ( 3.999999999999990674, -2.309401076758548221, -5.242734410091827613 ) ) ;
#4533=VERTEX_POINT ( 'NONE', #7090 ) ;
#4573=CARTESIAN_POINT ( 'NONE',  ( 2.099999999999999645, 0.000000000000000000, -0.2800830152838832965 ) ) ;
#4599=CARTESIAN_POINT ( 'NONE',  ( 1.155036213957052500E-14, 4.618802153517020059, -5.599999999999999645 ) ) ;
#4633=CARTESIAN_POINT ( 'NONE',  ( -4.000000000000000000, 1.935983797701054998, -0.2494693066162268769 ) ) ;
#4643=AXIS2_PLACEMENT_3D ( 'NONE', #14810, #5044, #9623 ) ;
#4656=LINE ( 'NONE', #20858, #9490 ) ;
#4681=DIRECTION ( 'NONE',  ( 1.000000000000000000, 0.000000000000000000, 0.000000000000000000 ) ) ;
#4687=DIRECTION ( 'NONE',  ( 0.000000000000000000, 0.000000000000000000, -1.000000000000000000 ) ) ;
#4695=ORIENTED_EDGE ( 'NONE', *, *, #14857, .F. ) ;
#4697=DIRECTION ( 'NONE',  ( -1.000000000000000000, 0.000000000000000000, 0.000000000000000000 ) ) ;
#4701=ORIENTED_EDGE ( 'NONE', *, *, #10454, .F. ) ;
#4713=CARTESIAN_POINT ( 'NONE',  ( 0.6543461111163461075, 4.241015250120812929, -0.1391502195351438376 ) ) ;
#4769=CARTESIAN_POINT ( 'NONE',  ( 4.000000000000004441, -1.549102112939112486, -0.1578953385959447620 ) ) ;
#4774=CARTESIAN_POINT ( 'NONE',  ( 0.000000000000000000, 0.000000000000000000, 0.000000000000000000 ) ) ;
#4789=ORIENTED_EDGE ( 'NONE', *, *, #10454, .T. ) ;
#4794=CARTESIAN_POINT ( 'NONE',  ( 4.000000000000004441, 0.7862748000878159171, -0.03447227762756879116 ) ) ;
#4839=EDGE_LOOP ( 'NONE', ( #8170, #6992, #11580, #5017 ) ) ;
#4841=DIRECTION ( 'NONE',  ( -0.000000000000000000, -0.000000000000000000, 1.000000000000000000 ) ) ;
#4863=CARTESIAN_POINT ( 'NONE',  ( 2.500000000000002220, 3.061616997868386099E-16, -5.574599999999999334 ) ) ;
#4877=AXIS2_PLACEMENT_3D ( 'NONE', #143, #16356, #17860 ) ;
#4886=CIRCLE ( 'NONE', #16725, 2.500000000000002220 ) ;
#4887=DIRECTION ( 'NONE',  ( -0.000000000000000000, -0.000000000000000000, 1.000000000000000000 ) ) ;
#4906=ORIENTED_EDGE ( 'NONE', *, *, #18663, .T. ) ;
#4918=CARTESIAN_POINT ( 'NONE',  ( 0.000000000000000000, 0.000000000000000000, -0.2800830152838832965 ) ) ;
#4943=ORIENTED_EDGE ( 'NONE', *, *, #13811, .T. ) ;
#4982=DIRECTION ( 'NONE',  ( -1.000000000000000000, 0.000000000000000000, 0.000000000000000000 ) ) ;
#5017=ORIENTED_EDGE ( 'NONE', *, *, #12781, .F. ) ;
#5038=VERTEX_POINT ( 'NONE', #10054 ) ;
#5044=DIRECTION ( 'NONE',  ( 0.000000000000000000, 0.000000000000000000, -1.000000000000000000 ) ) ;
#5094=ORIENTED_EDGE ( 'NONE', *, *, #15068, .T. ) ;
#5123=ADVANCED_FACE ( 'NONE', ( #2834 ), #3762, .T. ) ;
#5184=LINE ( 'NONE', #319, #15442 ) ;
#5189=EDGE_CURVE ( 'NONE', #520, #1320, #14861, .T. ) ;
#5215=CARTESIAN_POINT ( 'NONE',  ( 0.000000000000000000, 0.000000000000000000, -5.599999999999999645 ) ) ;
#5226=ORIENTED_EDGE ( 'NONE', *, *, #13261, .F. ) ;
#5228=EDGE_LOOP ( 'NONE', ( #17305, #8839, #20327, #2572, #9641, #6143 ) ) ;
#5234=CARTESIAN_POINT ( 'NONE',  ( -7.632783294297951215E-14, -4.618802153517020948, -0.3572655899081733644 ) ) ;
#5257=AXIS2_PLACEMENT_3D ( 'NONE', #17314, #15510, #2791 ) ;
#5259=DIRECTION ( 'NONE',  ( -0.000000000000000000, 0.000000000000000000, -1.000000000000000000 ) ) ;
#5262=ORIENTED_EDGE ( 'NONE', *, *, #17899, .F. ) ;
#5307=CIRCLE ( 'NONE', #19868, 2.099999999999999645 ) ;
#5315=CONICAL_SURFACE ( 'NONE', #11088, 4.000000000000000000, 1.047197551196595855 ) ;
#5319=CARTESIAN_POINT ( 'NONE',  ( -4.000000000000000000, -2.309401076758531346, -0.3572655899081733644 ) ) ;
#5323=DIRECTION ( 'NONE',  ( 1.000000000000000000, 0.000000000000000000, 0.000000000000000000 ) ) ;
#5364=ORIENTED_EDGE ( 'NONE', *, *, #17387, .F. ) ;
#5372=CARTESIAN_POINT ( 'NONE',  ( -1.321505333908964186, 3.855830693249140850, -5.565789719053469753 ) ) ;
#5430=ADVANCED_FACE ( 'NONE', ( #12220, #16889 ), #2364, .T. ) ;
#5460=AXIS2_PLACEMENT_3D ( 'NONE', #10794, #10691, #9302 ) ;
#5493=FACE_OUTER_BOUND ( 'NONE', #15007, .T. ) ;
#5504=CARTESIAN_POINT ( 'NONE',  ( 0.000000000000000000, 0.000000000000000000, 0.000000000000000000 ) ) ;
#5536=CARTESIAN_POINT ( 'NONE',  ( -4.000000000000000000, 0.3904826640788061631, -5.600000000000000533 ) ) ;
#5571=ORIENTED_EDGE ( 'NONE', *, *, #18940, .T. ) ;
#5637=LINE ( 'NONE', #16883, #12650 ) ;
#5671=AXIS2_PLACEMENT_3D ( 'NONE', #3475, #11451, #6559 ) ;
#5685=EDGE_CURVE ( 'NONE', #12949, #13448, #8667, .T. ) ;
#5694=DIRECTION ( 'NONE',  ( -0.8191520442889896891, 0.000000000000000000, -0.5735764363510490460 ) ) ;
#5704=EDGE_CURVE ( 'NONE', #20245, #12949, #6475, .T. ) ;
#5715=EDGE_CURVE ( 'NONE', #964, #12005, #14092, .T. ) ;
#5769=CARTESIAN_POINT ( 'NONE',  ( -4.000000000000000000, 2.309401076758531346, -5.242734410091827613 ) ) ;
#5818=AXIS2_PLACEMENT_3D ( 'NONE', #20454, #2661, #4121 ) ;
#5847=EDGE_CURVE ( 'NONE', #5038, #17353, #204, .T. ) ;
#5898=ORIENTED_EDGE ( 'NONE', *, *, #5704, .T. ) ;
#5907=FACE_OUTER_BOUND ( 'NONE', #8644, .T. ) ;
#6002=ORIENTED_EDGE ( 'NONE', *, *, #5189, .T. ) ;
#6009=EDGE_CURVE ( 'NONE', #20501, #8092, #12839, .T. ) ;
#6035=CARTESIAN_POINT ( 'NONE',  ( 0.3263565795980677420, -4.430380094434308802, -0.2484800633750392507 ) ) ;
#6052=DIRECTION ( 'NONE',  ( 0.8191520442889896891, 1.003171929053522158E-16, -0.5735764363510490460 ) ) ;
#6055=DIRECTION ( 'NONE',  ( -1.000000000000000000, 0.000000000000000000, 0.000000000000000000 ) ) ;
#6143=ORIENTED_EDGE ( 'NONE', *, *, #16419, .F. ) ;
#6179=CYLINDRICAL_SURFACE ( 'NONE', #9498, 2.099999999999999645 ) ;
#6309=ORIENTED_EDGE ( 'NONE', *, *, #12781, .T. ) ;
#6323=CARTESIAN_POINT ( 'NONE',  ( -4.000000000000000000, 1.557668341133497059, -0.1596965656957516910 ) ) ;
#6324=DIRECTION ( 'NONE',  ( -0.8191520442889896891, 1.003171929053522158E-16, 0.5735764363510490460 ) ) ;
#6347=AXIS2_PLACEMENT_3D ( 'NONE', #20288, #15427, #10868 ) ;
#6362=CARTESIAN_POINT ( 'NONE',  ( 4.000000000000003553, -0.7779732554280839318, -0.03354435108168055818 ) ) ;
#6391=DIRECTION ( 'NONE',  ( -0.5000000000000024425, 0.8660254037844372643, 0.000000000000000000 ) ) ;
#6408=ORIENTED_EDGE ( 'NONE', *, *, #15947, .F. ) ;
#6475=LINE ( 'NONE', #11470, #11042 ) ;
#6509=VERTEX_POINT ( 'NONE', #14195 ) ;
#6518=CARTESIAN_POINT ( 'NONE',  ( 0.000000000000000000, 0.000000000000000000, -5.574599999999999334 ) ) ;
#6559=DIRECTION ( 'NONE',  ( 1.000000000000000000, 0.000000000000000000, 0.000000000000000000 ) ) ;
#6583=CARTESIAN_POINT ( 'NONE',  ( 2.000000000000010658, -3.464101615137748169, 0.000000000000000000 ) ) ;
#6605=ADVANCED_FACE ( 'NONE', ( #19570 ), #237, .F. ) ;
#6613=ORIENTED_EDGE ( 'NONE', *, *, #19718, .T. ) ;
#6618=FACE_OUTER_BOUND ( 'NONE', #8087, .T. ) ;
#6624=CARTESIAN_POINT ( 'NONE',  ( -4.000000000000000000, 0.3904826640788011116, -3.430483436379915141E-17 ) ) ;
#6663=ORIENTED_EDGE ( 'NONE', *, *, #16497, .T. ) ;
#6682=FACE_OUTER_BOUND ( 'NONE', #14526, .T. ) ;
#6688=EDGE_LOOP ( 'NONE', ( #20302, #6002, #13742 ) ) ;
#6703=ORIENTED_EDGE ( 'NONE', *, *, #13811, .F. ) ;
#6708=DIRECTION ( 'NONE',  ( 1.000000000000000000, 0.000000000000000000, 0.000000000000000000 ) ) ;
#6729=CARTESIAN_POINT ( 'NONE',  ( -3.673643420401911275, -2.497823135841289677, -0.2484800633750114396 ) ) ;
#6761=EDGE_CURVE ( 'NONE', #1320, #20501, #1689, .T. ) ;
#6768=AXIS2_PLACEMENT_3D ( 'NONE', #7209, #10624, #4030 ) ;
#6772=DIRECTION ( 'NONE',  ( 0.000000000000000000, 0.000000000000000000, 1.000000000000000000 ) ) ;
#6781=CARTESIAN_POINT ( 'NONE',  ( -4.000000000000000000, -2.309401076758531346, -5.242734410091827613 ) ) ;
#6803=ORIENTED_EDGE ( 'NONE', *, *, #2332, .T. ) ;
#6886=EDGE_CURVE ( 'NONE', #9645, #4533, #12567, .T. ) ;
#6898=CARTESIAN_POINT ( 'NONE',  ( 4.000000000000003553, 0.3904826640788058856, -2.008738634413572465E-15 ) ) ;
#6904=CARTESIAN_POINT ( 'NONE',  ( 4.000000000000002665, 1.935983797701078313, -5.350530693383766412 ) ) ;
#6927=VERTEX_POINT ( 'NONE', #5769 ) ;
#6936=DIRECTION ( 'NONE',  ( -0.000000000000000000, -0.000000000000000000, 1.000000000000000000 ) ) ;
#6943=CARTESIAN_POINT ( 'NONE',  ( 3.673643420401900173, 2.497823135841254150, -5.351519936625005691 ) ) ;
#6952=ORIENTED_EDGE ( 'NONE', *, *, #12037, .T. ) ;
#6969=FACE_OUTER_BOUND ( 'NONE', #15455, .T. ) ;
#6987=ADVANCED_FACE ( 'NONE', ( #18828 ), #7720, .T. ) ;
#6992=ORIENTED_EDGE ( 'NONE', *, *, #16238, .F. ) ;
#7044=DIRECTION ( 'NONE',  ( -1.000000000000000000, 0.000000000000000000, 0.000000000000000000 ) ) ;
#7090=CARTESIAN_POINT ( 'NONE',  ( 4.000000000000000000, 0.000000000000000000, -5.600000000000000533 ) ) ;
#7104=CARTESIAN_POINT ( 'NONE',  ( 0.000000000000000000, 0.000000000000000000, -5.599999999999999645 ) ) ;
#7112=VERTEX_POINT ( 'NONE', #8005 ) ;
#7166=CARTESIAN_POINT ( 'NONE',  ( 1.084202172485504434E-14, 4.618802153517020059, -5.242734410091827613 ) ) ;
#7209=CARTESIAN_POINT ( 'NONE',  ( 0.000000000000000000, 0.000000000000000000, -5.599999999999999645 ) ) ;
#7227=CARTESIAN_POINT ( 'NONE',  ( 1.214306433183764966E-14, 4.618802153517020059, -5.599999999999999645 ) ) ;
#7231=CARTESIAN_POINT ( 'NONE',  ( -4.000000000000000000, 0.000000000000000000, -5.599999999999999645 ) ) ;
#7236=FILL_AREA_STYLE ('',( #789 ) ) ;
#7274=CARTESIAN_POINT ( 'NONE',  ( -1.318516776095820742, -3.857556137907092619, -5.599999999999983658 ) ) ;
#7275=ORIENTED_EDGE ( 'NONE', *, *, #3794, .F. ) ;
#7278=AXIS2_PLACEMENT_3D ( 'NONE', #19220, #12544, #4697 ) ;
#7325=AXIS2_PLACEMENT_3D ( 'NONE', #11915, #9069, #2492 ) ;
#7331=ORIENTED_EDGE ( 'NONE', *, *, #1173, .F. ) ;
#7350=PRESENTATION_STYLE_ASSIGNMENT (( #18595 ) ) ;
#7372=CARTESIAN_POINT ( 'NONE',  ( -4.000000000000000000, -1.933795701539610334, -5.351162342337702604 ) ) ;
#7430=DIRECTION ( 'NONE',  ( 0.000000000000000000, 0.000000000000000000, -1.000000000000000000 ) ) ;
#7434=VERTEX_POINT ( 'NONE', #9051 ) ;
#7458=DIRECTION ( 'NONE',  ( 0.8191520442889896891, 0.000000000000000000, 0.5735764363510490460 ) ) ;
#7462=DIRECTION ( 'NONE',  ( 0.8660254037844354880, -0.5000000000000055511, 0.000000000000000000 ) ) ;
#7500=CARTESIAN_POINT ( 'NONE',  ( -2.500000000000002220, 3.061616997868386099E-16, -5.600000000000000533 ) ) ;
#7509=ADVANCED_FACE ( 'NONE', ( #102 ), #18500, .T. ) ;
#7534=EDGE_CURVE ( 'NONE', #232, #5038, #20866, .T. ) ;
#7601=ORIENTED_EDGE ( 'NONE', *, *, #2496, .F. ) ;
#7643=LINE ( 'NONE', #2987, #18301 ) ;
#7648=ORIENTED_EDGE ( 'NONE', *, *, #12147, .F. ) ;
#7720=CONICAL_SURFACE ( 'NONE', #6347, 4.000000000000000000, 1.047197551196595855 ) ;
#7728=CARTESIAN_POINT ( 'NONE',  ( 2.678494666091051357, 3.072372537026354156, -0.03421028094653023183 ) ) ;
#7760=ADVANCED_FACE ( 'NONE', ( #6969 ), #17847, .F. ) ;
#7807=CARTESIAN_POINT ( 'NONE',  ( -2.500000000000002220, 0.000000000000000000, -5.574599999999999334 ) ) ;
#7834=PLANE ( 'NONE',  #8873 ) ;
#7870=AXIS2_PLACEMENT_3D ( 'NONE', #3489, #10282, #636 ) ;
#7913=ADVANCED_FACE ( 'NONE', ( #3862 ), #16801, .T. ) ;
#7917=CARTESIAN_POINT ( 'NONE',  ( -4.000000000000000000, 0.7862748000878058141, -0.03447227762756577968 ) ) ;
#7933=ADVANCED_FACE ( 'NONE', ( #12241 ), #735, .T. ) ;
#7937=PLANE ( 'NONE',  #1954 ) ;
#7959=STYLED_ITEM ( 'NONE', ( #8878 ), #14262 ) ;
#7969=CARTESIAN_POINT ( 'NONE',  ( -2.099999999999999645, 2.571758278209440971E-16, -5.599999999999999645 ) ) ;
#7973=PRODUCT_DEFINITION_FORMATION_WITH_SPECIFIED_SOURCE ( 'ANY', '', #13917, .NOT_KNOWN. ) ;
#7975=CARTESIAN_POINT ( 'NONE',  ( -2.681483223904239210, 3.070647092368425479, 2.604296331179000749E-15 ) ) ;
#7984=DIRECTION ( 'NONE',  ( -0.000000000000000000, -0.000000000000000000, 1.000000000000000000 ) ) ;
#8003=VERTEX_POINT ( 'NONE', #15315 ) ;
#8005=CARTESIAN_POINT ( 'NONE',  ( -7.459310946700270506E-14, -4.618802153517020948, -5.242734410091827613 ) ) ;
#8021=DIRECTION ( 'NONE',  ( -1.000000000000000000, -3.552713678800500929E-15, 0.000000000000000000 ) ) ;
#8087=EDGE_LOOP ( 'NONE', ( #5094, #1931, #16672, #5364 ) ) ;
#8092=VERTEX_POINT ( 'NONE', #20508 ) ;
#8098=ORIENTED_EDGE ( 'NONE', *, *, #5847, .F. ) ;
#8129=SHAPE_DEFINITION_REPRESENTATION ( #9997, #2344 ) ;
#8170=ORIENTED_EDGE ( 'NONE', *, *, #1077, .F. ) ;
#8171=CARTESIAN_POINT ( 'NONE',  ( -4.000000000000000000, 2.309401076758496263, -0.3572655899081631503 ) ) ;
#8178=CARTESIAN_POINT ( 'NONE',  ( 0.000000000000000000, 0.000000000000000000, -5.574599999999999334 ) ) ;
#8288=FACE_OUTER_BOUND ( 'NONE', #4839, .T. ) ;
#8454=ORIENTED_EDGE ( 'NONE', *, *, #18299, .T. ) ;
#8466=FACE_BOUND ( 'NONE', #17455, .T. ) ;
#8512=CARTESIAN_POINT ( 'NONE',  ( -2.678494666091065124, -3.072372537026387018, -5.565789719053451101 ) ) ;
#8521=CARTESIAN_POINT ( 'NONE',  ( 0.000000000000000000, 0.000000000000000000, 0.000000000000000000 ) ) ;
#8549=CARTESIAN_POINT ( 'NONE',  ( -1.660531772554312280, 3.660093687634848436, -5.600000000000003197 ) ) ;
#8567=VECTOR ( 'NONE', #20042, 1000.000000000000000 ) ;
#8574=CARTESIAN_POINT ( 'NONE',  ( -2.681483223904233881, 3.070647092368428588, -5.600000000000003197 ) ) ;
#8575=CARTESIAN_POINT ( 'NONE',  ( 0.6554360035617802227, -4.240386000424091861, -5.441324518471480687 ) ) ;
#8586=VERTEX_POINT ( 'NONE', #4429 ) ;
#8587=CIRCLE ( 'NONE', #4877, 2.500000000000000444 ) ;
#8602=CARTESIAN_POINT ( 'NONE',  ( 0.000000000000000000, 0.000000000000000000, -5.600000000000000533 ) ) ;
#8605=CARTESIAN_POINT ( 'NONE',  ( 2.099999999999999645, 0.000000000000000000, -5.294516984716111097 ) ) ;
#8644=EDGE_LOOP ( 'NONE', ( #2641, #19791, #9915 ) ) ;
#8667=CIRCLE ( 'NONE', #2921, 2.500000000000002220 ) ;
#8682=DIRECTION ( 'NONE',  ( -1.000000000000000000, 0.000000000000000000, 0.000000000000000000 ) ) ;
#8687=ORIENTED_EDGE ( 'NONE', *, *, #11678, .T. ) ;
#8717=VECTOR ( 'NONE', #6324, 1000.000000000000114 ) ;
#8729=CARTESIAN_POINT ( 'NONE',  ( -4.000000000000000000, 0.000000000000000000, 0.000000000000000000 ) ) ;
#8785=ORIENTED_EDGE ( 'NONE', *, *, #10809, .F. ) ;
#8792=EDGE_CURVE ( 'NONE', #17353, #9919, #9246, .T. ) ;
#8839=ORIENTED_EDGE ( 'NONE', *, *, #14857, .T. ) ;
#8840=DIRECTION ( 'NONE',  ( 0.000000000000000000, 0.000000000000000000, -1.000000000000000000 ) ) ;
#8848=CARTESIAN_POINT ( 'NONE',  ( 3.344563996438205677, 2.687817229851463097, -5.441324518471517102 ) ) ;
#8873=AXIS2_PLACEMENT_3D ( 'NONE', #12729, #14317, #20759 ) ;
#8878=PRESENTATION_STYLE_ASSIGNMENT (( #10586 ) ) ;
#8890=B_SPLINE_CURVE_WITH_KNOTS ( 'NONE', 3,
 ( #15228, #8549, #5372, #12056, #3988, #7166 ),
 .UNSPECIFIED., .F., .F.,
 ( 4, 2, 4 ),
 ( 0.002336974151641539946, 0.003500975885716448889, 0.004664977619791357832 ),
 .UNSPECIFIED. ) ;
#8967=CLOSED_SHELL ( 'NONE', ( #11767, #11652, #12202, #3741, #17012, #16911, #3006, #2471, #167, #7913, #20811, #1225, #5430, #18574, #18414, #5123, #7509, #13231, #6987, #10841, #16729, #7933, #12476, #18765, #949, #7760, #6605, #3292 ) ) ;
#8984=CONICAL_SURFACE ( 'NONE', #5257, 4.000000000000000000, 1.047197551196595855 ) ;
#9000=ORIENTED_EDGE ( 'NONE', *, *, #1952, .F. ) ;
#9051=CARTESIAN_POINT ( 'NONE',  ( 2.000000000000010658, -3.464101615137748169, 0.000000000000000000 ) ) ;
#9052=FACE_OUTER_BOUND ( 'NONE', #15495, .T. ) ;
#9059=( NAMED_UNIT ( * ) SI_UNIT ( $, .STERADIAN. ) SOLID_ANGLE_UNIT ( ) );
#9069=DIRECTION ( 'NONE',  ( -0.000000000000000000, -0.000000000000000000, 1.000000000000000000 ) ) ;
#9093=ORIENTED_EDGE ( 'NONE', *, *, #11345, .F. ) ;
#9232=CARTESIAN_POINT ( 'NONE',  ( 3.999999999999990674, -2.309401076758548221, -0.3572655899081733644 ) ) ;
#9246=CIRCLE ( 'NONE', #12972, 4.000000000000000888 ) ;
#9251=CARTESIAN_POINT ( 'NONE',  ( -4.000000000000000000, -2.309401076758525573, -5.599999999999999645 ) ) ;
#9302=DIRECTION ( 'NONE',  ( 1.000000000000000000, 0.000000000000000000, 0.000000000000000000 ) ) ;
#9346=AXIS2_PLACEMENT_3D ( 'NONE', #5504, #17075, #750 ) ;
#9361=AXIS2_PLACEMENT_3D ( 'NONE', #15165, #11982, #12187 ) ;
#9364=DIRECTION ( 'NONE',  ( -1.000000000000000000, 0.000000000000000000, 0.000000000000000000 ) ) ;
#9372=CARTESIAN_POINT ( 'NONE',  ( 1.084202172485504434E-14, 4.618802153517020059, -0.3572655899081733644 ) ) ;
#9450=LINE ( 'NONE', #7969, #9563 ) ;
#9478=CARTESIAN_POINT ( 'NONE',  ( 2.000000000000010658, -3.464101615137748169, -5.600000000000000533 ) ) ;
#9490=VECTOR ( 'NONE', #11218, 1000.000000000000000 ) ;
#9498=AXIS2_PLACEMENT_3D ( 'NONE', #5215, #11784, #18046 ) ;
#9499=CARTESIAN_POINT ( 'NONE',  ( -7.459310946700270506E-14, -4.618802153517020948, -5.242734410091827613 ) ) ;
#9503=CARTESIAN_POINT ( 'NONE',  ( -3.344563996438217224, -2.687817229851499068, -0.1586754815285013609 ) ) ;
#9504=CARTESIAN_POINT ( 'NONE',  ( -2.060000000000000941, 2.522772406243548923E-16, -0.3080913168122707546 ) ) ;
#9529=ORIENTED_EDGE ( 'NONE', *, *, #20237, .F. ) ;
#9532=ORIENTED_EDGE ( 'NONE', *, *, #18377, .F. ) ;
#9543=AXIS2_PLACEMENT_3D ( 'NONE', #15593, #7430, #6055 ) ;
#9563=VECTOR ( 'NONE', #12851, 1000.000000000000000 ) ;
#9623=DIRECTION ( 'NONE',  ( -1.000000000000000000, 0.000000000000000000, 0.000000000000000000 ) ) ;
#9641=ORIENTED_EDGE ( 'NONE', *, *, #14974, .F. ) ;
#9645=VERTEX_POINT ( 'NONE', #3507 ) ;
#9675=ORIENTED_EDGE ( 'NONE', *, *, #2765, .F. ) ;
#9690=CARTESIAN_POINT ( 'NONE',  ( 0.000000000000000000, 0.000000000000000000, -5.600000000000000533 ) ) ;
#9698=AXIS2_PLACEMENT_3D ( 'NONE', #9776, #13379, #1726 ) ;
#9709=CARTESIAN_POINT ( 'NONE',  ( -0.6543461111163950683, -4.241015250120822699, -0.1391502195351546900 ) ) ;
#9767=B_SPLINE_CURVE_WITH_KNOTS ( 'NONE', 3,
 ( #20643, #18758, #7728, #10703, #18865, #1055 ),
 .UNSPECIFIED., .F., .F.,
 ( 4, 2, 4 ),
 ( 0.002336974151641576809, 0.003500975885716453226, 0.004664977619791330077 ),
 .UNSPECIFIED. ) ;
#9776=CARTESIAN_POINT ( 'NONE',  ( 0.000000000000000000, 0.000000000000000000, -5.599999999999999645 ) ) ;
#9792=ORIENTED_EDGE ( 'NONE', *, *, #11741, .T. ) ;
#9799=ORIENTED_EDGE ( 'NONE', *, *, #11497, .F. ) ;
#9847=B_SPLINE_CURVE_WITH_KNOTS ( 'NONE', 3,
 ( #3695, #2119, #4206, #8575, #2629, #9499 ),
 .UNSPECIFIED., .F., .F.,
 ( 4, 2, 4 ),
 ( 0.002336974151641520864, 0.003500975885716454961, 0.004664977619791389057 ),
 .UNSPECIFIED. ) ;
#9848=CARTESIAN_POINT ( 'NONE',  ( 4.000000000000003553, -1.933795701539622103, -0.2488376576623028413 ) ) ;
#9851=DIRECTION ( 'NONE',  ( -1.000000000000000000, 0.000000000000000000, 0.000000000000000000 ) ) ;
#9915=ORIENTED_EDGE ( 'NONE', *, *, #5715, .T. ) ;
#9919=VERTEX_POINT ( 'NONE', #18568 ) ;
#9997=PRODUCT_DEFINITION_SHAPE ( 'NONE', 'NONE',  #15841 ) ;
#10038=EDGE_LOOP ( 'NONE', ( #4789, #17332, #15592 ) ) ;
#10051=ORIENTED_EDGE ( 'NONE', *, *, #13888, .F. ) ;
#10054=CARTESIAN_POINT ( 'NONE',  ( -4.000000000000000000, 0.000000000000000000, 0.000000000000000000 ) ) ;
#10103=EDGE_CURVE ( 'NONE', #14918, #2494, #16185, .T. ) ;
#10118=CARTESIAN_POINT ( 'NONE',  ( -4.000000000000000000, -2.309401076758531346, -5.242734410091827613 ) ) ;
#10126=DIRECTION ( 'NONE',  ( 1.000000000000000000, 0.000000000000000000, 0.000000000000000000 ) ) ;
#10160=CARTESIAN_POINT ( 'NONE',  ( 0.000000000000000000, 0.000000000000000000, 0.000000000000000000 ) ) ;
#10200=VECTOR ( 'NONE', #5694, 1000.000000000000114 ) ;
#10248=DIRECTION ( 'NONE',  ( 0.8660254037844371533, 0.5000000000000025535, 0.000000000000000000 ) ) ;
#10282=DIRECTION ( 'NONE',  ( 0.000000000000000000, 0.000000000000000000, -1.000000000000000000 ) ) ;
#10322=CARTESIAN_POINT ( 'NONE',  ( -4.000000000000000000, -0.3902508023145539462, 2.371692252312039717E-17 ) ) ;
#10369=ORIENTED_EDGE ( 'NONE', *, *, #16238, .T. ) ;
#10437=FACE_OUTER_BOUND ( 'NONE', #18672, .T. ) ;
#10447=DIRECTION ( 'NONE',  ( -0.5000000000000055511, -0.8660254037844354880, 0.000000000000000000 ) ) ;
#10454=EDGE_CURVE ( 'NONE', #964, #4388, #10882, .T. ) ;
#10567=ORIENTED_EDGE ( 'NONE', *, *, #1173, .T. ) ;
#10586=SURFACE_STYLE_USAGE ( .BOTH. , #3786 ) ;
#10589=MANIFOLD_SOLID_BREP ( 'EndChamfer', #8967 ) ;
#10618=CARTESIAN_POINT ( 'NONE',  ( -2.500000000000000444, 3.061616997868384127E-16, 3.469446951953614189E-15 ) ) ;
#10624=DIRECTION ( 'NONE',  ( 0.000000000000000000, 0.000000000000000000, 1.000000000000000000 ) ) ;
#10670=EDGE_CURVE ( 'NONE', #17353, #6509, #4304, .T. ) ;
#10691=DIRECTION ( 'NONE',  ( -0.000000000000000000, -0.000000000000000000, 1.000000000000000000 ) ) ;
#10703=CARTESIAN_POINT ( 'NONE',  ( 3.344563996438205677, 2.687817229851463097, -0.1586754815284831532 ) ) ;
#10768=CARTESIAN_POINT ( 'NONE',  ( 1.318516776095788545, 3.857556137907071747, 2.454790609853964971E-15 ) ) ;
#10780=ORIENTED_EDGE ( 'NONE', *, *, #18504, .F. ) ;
#10794=CARTESIAN_POINT ( 'NONE',  ( 0.000000000000000000, 0.000000000000000000, -5.600000000000000533 ) ) ;
#10809=EDGE_CURVE ( 'NONE', #15954, #20245, #4248, .T. ) ;
#10841=ADVANCED_FACE ( 'NONE', ( #9052 ), #8984, .T. ) ;
#10846=CARTESIAN_POINT ( 'NONE',  ( 0.000000000000000000, 0.000000000000000000, -5.294516984716111097 ) ) ;
#10868=DIRECTION ( 'NONE',  ( 1.000000000000000000, 0.000000000000000000, 0.000000000000000000 ) ) ;
#10882=B_SPLINE_CURVE_WITH_KNOTS ( 'NONE', 3,
 ( #13198, #16268, #8512, #14686, #481, #10118 ),
 .UNSPECIFIED., .F., .F.,
 ( 4, 2, 4 ),
 ( 0.002336974151641604130, 0.003500975885716476211, 0.004664977619791348291 ),
 .UNSPECIFIED. ) ;
#10884=CARTESIAN_POINT ( 'NONE',  ( 0.000000000000000000, 0.000000000000000000, -5.600000000000000533 ) ) ;
#10903=DIRECTION ( 'NONE',  ( 0.000000000000000000, 0.000000000000000000, 1.000000000000000000 ) ) ;
#10917=ORIENTED_EDGE ( 'NONE', *, *, #2765, .T. ) ;
#10931=CARTESIAN_POINT ( 'NONE',  ( 0.000000000000000000, 0.000000000000000000, -5.600000000000000533 ) ) ;
#10966=CARTESIAN_POINT ( 'NONE',  ( 1.084202172485504434E-14, 4.618802153517020059, -0.3572655899081733644 ) ) ;
#10968=ORIENTED_EDGE ( 'NONE', *, *, #13888, .T. ) ;
#11006=CARTESIAN_POINT ( 'NONE',  ( -4.000000000000000000, 2.309401076758496263, -5.599999999999999645 ) ) ;
#11042=VECTOR ( 'NONE', #17844, 1000.000000000000000 ) ;
#11088=AXIS2_PLACEMENT_3D ( 'NONE', #4774, #12947, #9851 ) ;
#11107=CARTESIAN_POINT ( 'NONE',  ( 1.084202172485504434E-14, 4.618802153517020059, -5.242734410091827613 ) ) ;
#11152=LINE ( 'NONE', #9251, #694 ) ;
#11167=ORIENTED_EDGE ( 'NONE', *, *, #2496, .T. ) ;
#11218=DIRECTION ( 'NONE',  ( 0.000000000000000000, 0.000000000000000000, 1.000000000000000000 ) ) ;
#11289=AXIS2_PLACEMENT_3D ( 'NONE', #4918, #20922, #6708 ) ;
#11342=ORIENTED_EDGE ( 'NONE', *, *, #8792, .F. ) ;
#11345=EDGE_CURVE ( 'NONE', #701, #17356, #5184, .T. ) ;
#11354=DIRECTION ( 'NONE',  ( 1.000000000000000000, 0.000000000000000000, 0.000000000000000000 ) ) ;
#11370=( GEOMETRIC_REPRESENTATION_CONTEXT ( 3 ) GLOBAL_UNCERTAINTY_ASSIGNED_CONTEXT ( ( #2213 ) ) GLOBAL_UNIT_ASSIGNED_CONTEXT ( ( #2484, #17109, #9059 ) ) REPRESENTATION_CONTEXT ( 'NONE', 'WORKASPACE' ) );
#11407=EDGE_CURVE ( 'NONE', #12005, #7112, #9847, .T. ) ;
#11451=DIRECTION ( 'NONE',  ( -0.000000000000000000, -0.000000000000000000, 1.000000000000000000 ) ) ;
#11463=ORIENTED_EDGE ( 'NONE', *, *, #10103, .T. ) ;
#11464=DIRECTION ( 'NONE',  ( -1.000000000000000000, 0.000000000000000000, 0.000000000000000000 ) ) ;
#11470=CARTESIAN_POINT ( 'NONE',  ( 2.500000000000002220, 0.000000000000000000, -25.03750572909317285 ) ) ;
#11496=CARTESIAN_POINT ( 'NONE',  ( -1.318516776095821186, -3.857556137907092175, -1.739862437281285109E-14 ) ) ;
#11497=EDGE_CURVE ( 'NONE', #1320, #8003, #12053, .T. ) ;
#11502=CARTESIAN_POINT ( 'NONE',  ( -4.000000000000000000, 2.309401076758496263, -0.3572655899081631503 ) ) ;
#11511=PRODUCT_CONTEXT ( 'NONE', #11824, 'mechanical' ) ;
#11580=ORIENTED_EDGE ( 'NONE', *, *, #11345, .T. ) ;
#11608=DIRECTION ( 'NONE',  ( -1.000000000000000000, 0.000000000000000000, 0.000000000000000000 ) ) ;
#11652=ADVANCED_FACE ( 'NONE', ( #6618 ), #1590, .F. ) ;
#11678=EDGE_CURVE ( 'NONE', #2494, #9919, #18153, .T. ) ;
#11682=DIRECTION ( 'NONE',  ( 1.000000000000000000, 0.000000000000000000, 0.000000000000000000 ) ) ;
#11698=ORIENTED_EDGE ( 'NONE', *, *, #15336, .F. ) ;
#11732=AXIS2_PLACEMENT_3D ( 'NONE', #10160, #16414, #4982 ) ;
#11741=EDGE_CURVE ( 'NONE', #17356, #988, #13939, .T. ) ;
#11767=ADVANCED_FACE ( 'NONE', ( #15207 ), #12235, .F. ) ;
#11784=DIRECTION ( 'NONE',  ( 0.000000000000000000, 0.000000000000000000, 1.000000000000000000 ) ) ;
#11787=CARTESIAN_POINT ( 'NONE',  ( -4.000000000000000000, -1.933795701539610556, -0.2488376576622980119 ) ) ;
#11824=APPLICATION_CONTEXT ( 'automotive_design' ) ;
#11870=ORIENTED_EDGE ( 'NONE', *, *, #1077, .T. ) ;
#11896=AXIS2_PLACEMENT_3D ( 'NONE', #3968, #8840, #7044 ) ;
#11913=CIRCLE ( 'NONE', #2789, 4.000000000000000888 ) ;
#11915=CARTESIAN_POINT ( 'NONE',  ( 0.000000000000000000, 0.000000000000000000, -25.03750572909317285 ) ) ;
#11958=( NAMED_UNIT ( * ) SI_UNIT ( $, .STERADIAN. ) SOLID_ANGLE_UNIT ( ) );
#11982=DIRECTION ( 'NONE',  ( -0.000000000000000000, 0.000000000000000000, -1.000000000000000000 ) ) ;
#12005=VERTEX_POINT ( 'NONE', #9478 ) ;
#12037=EDGE_CURVE ( 'NONE', #6509, #9919, #2599, .T. ) ;
#12053=CIRCLE ( 'NONE', #16453, 4.000000000000000888 ) ;
#12056=CARTESIAN_POINT ( 'NONE',  ( -0.6554360035617894376, 4.240386000424038571, -5.441324518471509997 ) ) ;
#12057=VERTEX_POINT ( 'NONE', #17229 ) ;
#12127=SURFACE_SIDE_STYLE ('',( #20168 ) ) ;
#12147=EDGE_CURVE ( 'NONE', #988, #15454, #8587, .T. ) ;
#12187=DIRECTION ( 'NONE',  ( -1.000000000000000000, 0.000000000000000000, 0.000000000000000000 ) ) ;
#12202=ADVANCED_FACE ( 'NONE', ( #19743 ), #3843, .F. ) ;
#12203=CONICAL_SURFACE ( 'NONE', #14917, 4.000000000000000000, 1.047197551196595855 ) ;
#12220=FACE_BOUND ( 'NONE', #19261, .T. ) ;
#12223=CARTESIAN_POINT ( 'NONE',  ( -4.000000000000000000, 0.7862748000878172494, -5.565527722372433317 ) ) ;
#12235=CYLINDRICAL_SURFACE ( 'NONE', #7325, 2.500000000000002220 ) ;
#12241=FACE_OUTER_BOUND ( 'NONE', #1026, .T. ) ;
#12278=( NAMED_UNIT ( * ) PLANE_ANGLE_UNIT ( ) SI_UNIT ( $, .RADIAN. ) );
#12322=ORIENTED_EDGE ( 'NONE', *, *, #6009, .F. ) ;
#12324=FACE_OUTER_BOUND ( 'NONE', #18313, .T. ) ;
#12405=DIRECTION ( 'NONE',  ( -1.000000000000000000, 0.000000000000000000, 0.000000000000000000 ) ) ;
#12430=DIRECTION ( 'NONE',  ( -1.000000000000000000, 0.000000000000000000, 0.000000000000000000 ) ) ;
#12461=AXIS2_PLACEMENT_3D ( 'NONE', #19474, #3361, #185 ) ;
#12476=ADVANCED_FACE ( 'NONE', ( #12324 ), #19441, .T. ) ;
#12485=CONICAL_SURFACE ( 'NONE', #17903, 4.000000000000000000, 1.047197551196595855 ) ;
#12528=ORIENTED_EDGE ( 'NONE', *, *, #6761, .T. ) ;
#12544=DIRECTION ( 'NONE',  ( 0.000000000000000000, -0.000000000000000000, 1.000000000000000000 ) ) ;
#12558=CARTESIAN_POINT ( 'NONE',  ( 2.000000000000027089, 3.464101615137739731, 0.000000000000000000 ) ) ;
#12567=B_SPLINE_CURVE_WITH_KNOTS ( 'NONE', 3,
 ( #4507, #17451, #19032, #12684, #15528, #18933 ),
 .UNSPECIFIED., .F., .F.,
 ( 4, 2, 4 ),
 ( 0.004120275011746849653, 0.005288420935197133549, 0.006456566858647417445 ),
 .UNSPECIFIED. ) ;
#12608=FACE_OUTER_BOUND ( 'NONE', #13568, .T. ) ;
#12639=CARTESIAN_POINT ( 'NONE',  ( -2.000000000000009770, 3.464101615137749057, 0.000000000000000000 ) ) ;
#12650=VECTOR ( 'NONE', #2044, 1000.000000000000000 ) ;
#12651=DIRECTION ( 'NONE',  ( -1.000000000000000000, 0.000000000000000000, 0.000000000000000000 ) ) ;
#12665=CARTESIAN_POINT ( 'NONE',  ( -2.000000000000009770, 3.464101615137749057, 0.000000000000000000 ) ) ;
#12684=CARTESIAN_POINT ( 'NONE',  ( 4.000000000000003553, -0.7779732554280840429, -5.566455648918319454 ) ) ;
#12707=ORIENTED_EDGE ( 'NONE', *, *, #20199, .F. ) ;
#12717=ORIENTED_EDGE ( 'NONE', *, *, #2084, .T. ) ;
#12729=CARTESIAN_POINT ( 'NONE',  ( 4.000000000000003553, 2.309401076758480720, -5.599999999999999645 ) ) ;
#12735=ORIENTED_EDGE ( 'NONE', *, *, #2205, .T. ) ;
#12747=FACE_OUTER_BOUND ( 'NONE', #1558, .T. ) ;
#12750=( GEOMETRIC_REPRESENTATION_CONTEXT ( 3 ) GLOBAL_UNCERTAINTY_ASSIGNED_CONTEXT ( ( #526 ) ) GLOBAL_UNIT_ASSIGNED_CONTEXT ( ( #19696, #12278, #18754 ) ) REPRESENTATION_CONTEXT ( 'NONE', 'WORKASPACE' ) );
#12777=DIRECTION ( 'NONE',  ( -0.8660254037844372643, -0.5000000000000024425, 0.000000000000000000 ) ) ;
#12781=EDGE_CURVE ( 'NONE', #12057, #17356, #5307, .T. ) ;
#12839=LINE ( 'NONE', #4355, #2243 ) ;
#12851=DIRECTION ( 'NONE',  ( 0.000000000000000000, 0.000000000000000000, 1.000000000000000000 ) ) ;
#12908=CARTESIAN_POINT ( 'NONE',  ( 0.6543461111163461075, 4.241015250120812929, -5.460849780464856806 ) ) ;
#12947=DIRECTION ( 'NONE',  ( 0.000000000000000000, 0.000000000000000000, -1.000000000000000000 ) ) ;
#12949=VERTEX_POINT ( 'NONE', #4863 ) ;
#12955=CARTESIAN_POINT ( 'NONE',  ( -2.000000000000009770, 3.464101615137749057, 0.000000000000000000 ) ) ;
#12972=AXIS2_PLACEMENT_3D ( 'NONE', #19777, #5259, #18199 ) ;
#13067=EDGE_CURVE ( 'NONE', #8003, #520, #8890, .T. ) ;
#13085=ORIENTED_EDGE ( 'NONE', *, *, #18940, .F. ) ;
#13109=CARTESIAN_POINT ( 'NONE',  ( 2.500000000000002220, 0.000000000000000000, -5.600000000000000533 ) ) ;
#13135=ORIENTED_EDGE ( 'NONE', *, *, #2892, .F. ) ;
#13165=B_SPLINE_CURVE_WITH_KNOTS ( 'NONE', 3,
 ( #18439, #13360, #8574, #18126 ),
 .UNSPECIFIED., .F., .F.,
 ( 4, 4 ),
 ( 2.380737581782212780E-07, 0.002336974151641539946 ),
 .UNSPECIFIED. ) ;
#13198=CARTESIAN_POINT ( 'NONE',  ( -2.000000000000022649, -3.464101615137742396, -5.600000000000000533 ) ) ;
#13231=ADVANCED_FACE ( 'NONE', ( #5907 ), #18886, .T. ) ;
#13261=EDGE_CURVE ( 'NONE', #7112, #964, #13707, .T. ) ;
#13317=EDGE_LOOP ( 'NONE', ( #6663, #15837, #13883, #18918, #4701, #5226 ) ) ;
#13360=CARTESIAN_POINT ( 'NONE',  ( -3.345653888883663996, 2.687187980154699840, -5.460849780464863024 ) ) ;
#13379=DIRECTION ( 'NONE',  ( 0.000000000000000000, -0.000000000000000000, 1.000000000000000000 ) ) ;
#13401=EDGE_CURVE ( 'NONE', #12057, #15454, #1363, .T. ) ;
#13431=CARTESIAN_POINT ( 'NONE',  ( 4.000000000000003553, 2.309401076758524685, -5.242734410091827613 ) ) ;
#13448=VERTEX_POINT ( 'NONE', #7807 ) ;
#13491=FACE_OUTER_BOUND ( 'NONE', #6688, .T. ) ;
#13499=LINE ( 'NONE', #663, #8567 ) ;
#13568=EDGE_LOOP ( 'NONE', ( #17281, #11870, #9000, #9093 ) ) ;
#13695=DIRECTION ( 'NONE',  ( -1.000000000000000000, 1.776356839400250465E-15, 0.000000000000000000 ) ) ;
#13707=B_SPLINE_CURVE_WITH_KNOTS ( 'NONE', 3,
 ( #19050, #15339, #7274, #18623 ),
 .UNSPECIFIED., .F., .F.,
 ( 4, 4 ),
 ( 2.380737582480036903E-07, 0.002336974151641604130 ),
 .UNSPECIFIED. ) ;
#13709=DIRECTION ( 'NONE',  ( 0.000000000000000000, 0.000000000000000000, -1.000000000000000000 ) ) ;
#13714=CARTESIAN_POINT ( 'NONE',  ( -4.000000000000000000, 1.557668341133520373, -5.440303434304243346 ) ) ;
#13742=ORIENTED_EDGE ( 'NONE', *, *, #11497, .T. ) ;
#13769=DIRECTION ( 'NONE',  ( 1.000000000000000000, 0.000000000000000000, 0.000000000000000000 ) ) ;
#13784=CARTESIAN_POINT ( 'NONE',  ( 2.000000000000010658, -3.464101615137748169, 0.000000000000000000 ) ) ;
#13811=EDGE_CURVE ( 'NONE', #9645, #12005, #17443, .T. ) ;
#13816=ORIENTED_EDGE ( 'NONE', *, *, #10670, .T. ) ;
#13849=CARTESIAN_POINT ( 'NONE',  ( -4.000000000000000000, -0.3902508023145548899, -5.600000000000000533 ) ) ;
#13883=ORIENTED_EDGE ( 'NONE', *, *, #20237, .T. ) ;
#13887=EDGE_LOOP ( 'NONE', ( #15639, #15225, #5898, #19994 ) ) ;
#13888=EDGE_CURVE ( 'NONE', #7434, #232, #2263, .T. ) ;
#13917=PRODUCT ( 'hex nut gradec_iso_ISO - 4034 - M5 - N', 'hex nut gradec_iso_ISO - 4034 - M5 - N', '', ( #11511 ) ) ;
#13939=LINE ( 'NONE', #18710, #15796 ) ;
#13942=CONICAL_SURFACE ( 'NONE', #9543, 4.000000000000000000, 1.047197551196595855 ) ;
#13958=CIRCLE ( 'NONE', #5818, 4.000000000000000888 ) ;
#13966=DIRECTION ( 'NONE',  ( 1.000000000000000000, 0.000000000000000000, 0.000000000000000000 ) ) ;
#14036=ORIENTED_EDGE ( 'NONE', *, *, #13401, .T. ) ;
#14080=ORIENTED_EDGE ( 'NONE', *, *, #11678, .F. ) ;
#14092=CIRCLE ( 'NONE', #9698, 4.000000000000000888 ) ;
#14100=ORIENTED_EDGE ( 'NONE', *, *, #6761, .F. ) ;
#14112=ORIENTED_EDGE ( 'NONE', *, *, #2205, .F. ) ;
#14129=ORIENTED_EDGE ( 'NONE', *, *, #5189, .F. ) ;
#14190=CYLINDRICAL_SURFACE ( 'NONE', #2117, 2.500000000000002220 ) ;
#14195=CARTESIAN_POINT ( 'NONE',  ( 1.084202172485504434E-14, 4.618802153517020059, -0.3572655899081733644 ) ) ;
#14246=CARTESIAN_POINT ( 'NONE',  ( -0.6554360035617894376, 4.240386000424038571, -0.1586754815284913411 ) ) ;
#14262=ADVANCED_BREP_SHAPE_REPRESENTATION ( '', ( #10589, #12461 ), #12750 ) ;
#14317=DIRECTION ( 'NONE',  ( 0.5000000000000066613, 0.8660254037844348218, -0.000000000000000000 ) ) ;
#14441=MECHANICAL_DESIGN_GEOMETRIC_PRESENTATION_REPRESENTATION('',(#7959),#14758);
#14526=EDGE_LOOP ( 'NONE', ( #16512, #7275, #18798, #201, #3015, #11698 ) ) ;
#14585=LINE ( 'NONE', #17876, #1798 ) ;
#14640=PLANE ( 'NONE',  #4191 ) ;
#14646=DIRECTION ( 'NONE',  ( 1.000000000000000000, 0.000000000000000000, 0.000000000000000000 ) ) ;
#14659=PLANE ( 'NONE',  #3391 ) ;
#14686=CARTESIAN_POINT ( 'NONE',  ( -3.344563996438217224, -2.687817229851499068, -5.441324518471498450 ) ) ;
#14698=CARTESIAN_POINT ( 'NONE',  ( -2.678494666091065124, -3.072372537026387018, -0.03421028094655000767 ) ) ;
#14724=ORIENTED_EDGE ( 'NONE', *, *, #8792, .T. ) ;
#14758=( GEOMETRIC_REPRESENTATION_CONTEXT ( 3 ) GLOBAL_UNCERTAINTY_ASSIGNED_CONTEXT ( ( #15558 ) ) GLOBAL_UNIT_ASSIGNED_CONTEXT ( ( #18543, #15555, #11958 ) ) REPRESENTATION_CONTEXT ( 'NONE', 'WORKASPACE' ) );
#14790=EDGE_LOOP ( 'NONE', ( #12528, #9532, #6613 ) ) ;
#14810=CARTESIAN_POINT ( 'NONE',  ( 0.000000000000000000, 0.000000000000000000, -5.574599999999999334 ) ) ;
#14840=CARTESIAN_POINT ( 'NONE',  ( 4.000000000000000000, 0.000000000000000000, 0.000000000000000000 ) ) ;
#14846=DIRECTION ( 'NONE',  ( -0.000000000000000000, 0.000000000000000000, -1.000000000000000000 ) ) ;
#14857=EDGE_CURVE ( 'NONE', #19414, #5038, #20423, .T. ) ;
#14861=B_SPLINE_CURVE_WITH_KNOTS ( 'NONE', 3,
 ( #11107, #12908, #3149, #16190 ),
 .UNSPECIFIED., .F., .F.,
 ( 4, 4 ),
 ( 2.380737581618758185E-07, 0.002336974151641576809 ),
 .UNSPECIFIED. ) ;
#14917=AXIS2_PLACEMENT_3D ( 'NONE', #8602, #760, #869 ) ;
#14918=VERTEX_POINT ( 'NONE', #16781 ) ;
#14957=CARTESIAN_POINT ( 'NONE',  ( 2.000000000000010658, -3.464101615137748169, -5.600000000000000533 ) ) ;
#14961=DIRECTION ( 'NONE',  ( -0.000000000000000000, -0.000000000000000000, 1.000000000000000000 ) ) ;
#14974=EDGE_CURVE ( 'NONE', #8586, #6927, #711, .T. ) ;
#15007=EDGE_LOOP ( 'NONE', ( #8098, #18476, #10051, #7331, #8687, #11342 ) ) ;
#15068=EDGE_CURVE ( 'NONE', #1492, #701, #2851, .T. ) ;
#15096=B_SPLINE_CURVE_WITH_KNOTS ( 'NONE', 3,
 ( #16339, #1829, #3317, #6583 ),
 .UNSPECIFIED., .F., .F.,
 ( 4, 4 ),
 ( 2.380737581781750353E-07, 0.002336974151641521731 ),
 .UNSPECIFIED. ) ;
#15124=CARTESIAN_POINT ( 'NONE',  ( 0.000000000000000000, 0.000000000000000000, -5.294516984716111097 ) ) ;
#15165=CARTESIAN_POINT ( 'NONE',  ( 0.000000000000000000, 0.000000000000000000, 0.000000000000000000 ) ) ;
#15177=CARTESIAN_POINT ( 'NONE',  ( 4.000000000000003553, 2.309401076758524685, -5.242734410091827613 ) ) ;
#15207=FACE_OUTER_BOUND ( 'NONE', #4502, .T. ) ;
#15225=ORIENTED_EDGE ( 'NONE', *, *, #2332, .F. ) ;
#15226=EDGE_CURVE ( 'NONE', #14918, #7434, #15096, .T. ) ;
#15228=CARTESIAN_POINT ( 'NONE',  ( -2.000000000000009770, 3.464101615137749057, -5.600000000000000533 ) ) ;
#15241=FILL_AREA_STYLE_COLOUR ( '', #3582 ) ;
#15315=CARTESIAN_POINT ( 'NONE',  ( -2.000000000000009770, 3.464101615137749057, -5.600000000000000533 ) ) ;
#15317=B_SPLINE_CURVE_WITH_KNOTS ( 'NONE', 3,
 ( #926, #7372, #2820, #17135, #13849, #20294 ),
 .UNSPECIFIED., .F., .F.,
 ( 4, 2, 4 ),
 ( 0.004120275011746843581, 0.005288420935197119671, 0.006456566858647394894 ),
 .UNSPECIFIED. ) ;
#15336=EDGE_CURVE ( 'NONE', #2494, #8092, #17885, .T. ) ;
#15339=CARTESIAN_POINT ( 'NONE',  ( -0.6543461111163939581, -4.241015250120822699, -5.460849780464846148 ) ) ;
#15427=DIRECTION ( 'NONE',  ( -0.000000000000000000, -0.000000000000000000, 1.000000000000000000 ) ) ;
#15442=VECTOR ( 'NONE', #6772, 1000.000000000000000 ) ;
#15454=VERTEX_POINT ( 'NONE', #10618 ) ;
#15455=EDGE_LOOP ( 'NONE', ( #19720, #6309, #9792, #2020 ) ) ;
#15478=ORIENTED_EDGE ( 'NONE', *, *, #6886, .F. ) ;
#15495=EDGE_LOOP ( 'NONE', ( #16704, #4695, #9529 ) ) ;
#15501=DIRECTION ( 'NONE',  ( 0.000000000000000000, -0.000000000000000000, 1.000000000000000000 ) ) ;
#15510=DIRECTION ( 'NONE',  ( 0.000000000000000000, 0.000000000000000000, -1.000000000000000000 ) ) ;
#15528=CARTESIAN_POINT ( 'NONE',  ( 4.000000000000003553, -0.3902508023145557225, -5.599999999999998757 ) ) ;
#15555=( NAMED_UNIT ( * ) PLANE_ANGLE_UNIT ( ) SI_UNIT ( $, .RADIAN. ) );
#15558=UNCERTAINTY_MEASURE_WITH_UNIT (LENGTH_MEASURE( 1.000000000000000082E-05 ), #18543, 'distance_accuracy_value', 'NONE');
#15591=CIRCLE ( 'NONE', #1054, 4.000000000000000888 ) ;
#15592=ORIENTED_EDGE ( 'NONE', *, *, #2892, .T. ) ;
#15593=CARTESIAN_POINT ( 'NONE',  ( 0.000000000000000000, 0.000000000000000000, 0.000000000000000000 ) ) ;
#15639=ORIENTED_EDGE ( 'NONE', *, *, #2084, .F. ) ;
#15783=AXIS2_PLACEMENT_3D ( 'NONE', #10884, #2721, #13966 ) ;
#15785=DIRECTION ( 'NONE',  ( 1.000000000000000000, 0.000000000000000000, 0.000000000000000000 ) ) ;
#15796=VECTOR ( 'NONE', #7458, 1000.000000000000114 ) ;
#15816=CARTESIAN_POINT ( 'NONE',  ( 0.000000000000000000, 0.000000000000000000, -5.600000000000000533 ) ) ;
#15819=CARTESIAN_POINT ( 'NONE',  ( 4.000000000000003553, 2.309401076758524685, -5.242734410091827613 ) ) ;
#15829=VECTOR ( 'NONE', #4373, 1000.000000000000000 ) ;
#15837=ORIENTED_EDGE ( 'NONE', *, *, #17899, .T. ) ;
#15841=PRODUCT_DEFINITION ( 'UNKNOWN', '', #7973, #16843 ) ;
#15885=CYLINDRICAL_SURFACE ( 'NONE', #6768, 2.099999999999999645 ) ;
#15947=EDGE_CURVE ( 'NONE', #9919, #8092, #9767, .T. ) ;
#15954=VERTEX_POINT ( 'NONE', #7500 ) ;
#15969=FACE_OUTER_BOUND ( 'NONE', #13887, .T. ) ;
#16030=CARTESIAN_POINT ( 'NONE',  ( -4.000000000000000000, 2.309401076758496263, -5.599999999999999645 ) ) ;
#16102=COLOUR_RGB ( '', 0.09019608, 0.27058824, 0.51372549) ;
#16136=CIRCLE ( 'NONE', #225, 4.000000000000000000 ) ;
#16185=B_SPLINE_CURVE_WITH_KNOTS ( 'NONE', 3,
 ( #9232, #9848, #4769, #6362, #1808, #14840 ),
 .UNSPECIFIED., .F., .F.,
 ( 4, 2, 4 ),
 ( 0.004120275011746849653, 0.005288420935197133549, 0.006456566858647416578 ),
 .UNSPECIFIED. ) ;
#16190=CARTESIAN_POINT ( 'NONE',  ( 2.000000000000027089, 3.464101615137739731, -5.600000000000000533 ) ) ;
#16238=EDGE_CURVE ( 'NONE', #701, #1492, #18026, .T. ) ;
#16254=CARTESIAN_POINT ( 'NONE',  ( -4.000000000000000000, 2.309401076758496263, -0.3572655899081631503 ) ) ;
#16268=CARTESIAN_POINT ( 'NONE',  ( -2.339468227445729021, -3.268109542640674547, -5.599999999999982769 ) ) ;
#16276=CARTESIAN_POINT ( 'NONE',  ( -2.000000000000022649, -3.464101615137742396, 0.000000000000000000 ) ) ;
#16296=ORIENTED_EDGE ( 'NONE', *, *, #5685, .F. ) ;
#16301=AXIS2_PLACEMENT_3D ( 'NONE', #20073, #10447, #7462 ) ;
#16333=CARTESIAN_POINT ( 'NONE',  ( 3.345653888883671545, -2.687187980154741140, -5.460849780464844372 ) ) ;
#16339=CARTESIAN_POINT ( 'NONE',  ( 3.999999999999990674, -2.309401076758548221, -0.3572655899081733644 ) ) ;
#16356=DIRECTION ( 'NONE',  ( -0.000000000000000000, -0.000000000000000000, 1.000000000000000000 ) ) ;
#16373=EDGE_LOOP ( 'NONE', ( #14724, #17207, #20830 ) ) ;
#16414=DIRECTION ( 'NONE',  ( -0.000000000000000000, 0.000000000000000000, -1.000000000000000000 ) ) ;
#16419=EDGE_CURVE ( 'NONE', #4388, #8586, #15317, .T. ) ;
#16453=AXIS2_PLACEMENT_3D ( 'NONE', #20723, #1567, #8021 ) ;
#16497=EDGE_CURVE ( 'NONE', #7112, #17615, #14585, .T. ) ;
#16512=ORIENTED_EDGE ( 'NONE', *, *, #10103, .F. ) ;
#16558=DIRECTION ( 'NONE',  ( 1.000000000000000000, 0.000000000000000000, 0.000000000000000000 ) ) ;
#16672=ORIENTED_EDGE ( 'NONE', *, *, #18299, .F. ) ;
#16704=ORIENTED_EDGE ( 'NONE', *, *, #7534, .T. ) ;
#16725=AXIS2_PLACEMENT_3D ( 'NONE', #19735, #19427, #11682 ) ;
#16729=ADVANCED_FACE ( 'NONE', ( #10437 ), #1048, .T. ) ;
#16758=STYLED_ITEM ( 'NONE', ( #7350 ), #10589 ) ;
#16781=CARTESIAN_POINT ( 'NONE',  ( 3.999999999999990674, -2.309401076758548221, -0.3572655899081733644 ) ) ;
#16801=PLANE ( 'NONE',  #16301 ) ;
#16823=CARTESIAN_POINT ( 'NONE',  ( -2.271448787322325728E-15, -4.618802153517061804, -5.599999999999999645 ) ) ;
#16843=PRODUCT_DEFINITION_CONTEXT ( 'detailed design', #316, 'design' ) ;
#16883=CARTESIAN_POINT ( 'NONE',  ( -2.500000000000002220, 3.061616997868386099E-16, -25.03750572909317285 ) ) ;
#16889=FACE_OUTER_BOUND ( 'NONE', #20720, .T. ) ;
#16895=CIRCLE ( 'NONE', #1347, 2.500000000000000444 ) ;
#16899=DIRECTION ( 'NONE',  ( 0.000000000000000000, 0.000000000000000000, -1.000000000000000000 ) ) ;
#16911=ADVANCED_FACE ( 'NONE', ( #3411 ), #14659, .T. ) ;
#16936=SHAPE_REPRESENTATION_RELATIONSHIP ( 'NONE' , 'NONE' ,  #2344, #14262 ) ;
#17012=ADVANCED_FACE ( 'NONE', ( #8288 ), #6179, .F. ) ;
#17075=DIRECTION ( 'NONE',  ( -0.000000000000000000, 0.000000000000000000, -1.000000000000000000 ) ) ;
#17085=CARTESIAN_POINT ( 'NONE',  ( 4.000000000000004441, 0.7862748000878170274, -5.565527722372433317 ) ) ;
#17109=( NAMED_UNIT ( * ) PLANE_ANGLE_UNIT ( ) SI_UNIT ( $, .RADIAN. ) );
#17135=CARTESIAN_POINT ( 'NONE',  ( -4.000000000000000000, -0.7779732554280797130, -5.566455648918322119 ) ) ;
#17186=ORIENTED_EDGE ( 'NONE', *, *, #1340, .T. ) ;
#17207=ORIENTED_EDGE ( 'NONE', *, *, #12037, .F. ) ;
#17218=ORIENTED_EDGE ( 'NONE', *, *, #18663, .F. ) ;
#17229=CARTESIAN_POINT ( 'NONE',  ( -2.099999999999999645, 2.571758278209440971E-16, -0.2800830152838832965 ) ) ;
#17281=ORIENTED_EDGE ( 'NONE', *, *, #15068, .F. ) ;
#17305=ORIENTED_EDGE ( 'NONE', *, *, #4188, .T. ) ;
#17314=CARTESIAN_POINT ( 'NONE',  ( 0.000000000000000000, 0.000000000000000000, 0.000000000000000000 ) ) ;
#17332=ORIENTED_EDGE ( 'NONE', *, *, #16419, .T. ) ;
#17353=VERTEX_POINT ( 'NONE', #12639 ) ;
#17356=VERTEX_POINT ( 'NONE', #4573 ) ;
#17387=EDGE_CURVE ( 'NONE', #1492, #13448, #20780, .T. ) ;
#17443=B_SPLINE_CURVE_WITH_KNOTS ( 'NONE', 3,
 ( #2025, #16333, #1634, #14957 ),
 .UNSPECIFIED., .F., .F.,
 ( 4, 4 ),
 ( 2.380737581782212780E-07, 0.002336974151641520864 ),
 .UNSPECIFIED. ) ;
#17451=CARTESIAN_POINT ( 'NONE',  ( 4.000000000000003553, -1.933795701539621659, -5.351162342337697275 ) ) ;
#17455=EDGE_LOOP ( 'NONE', ( #7648, #17218 ) ) ;
#17482=DIRECTION ( 'NONE',  ( -1.000000000000000000, 0.000000000000000000, 0.000000000000000000 ) ) ;
#17575=CARTESIAN_POINT ( 'NONE',  ( -2.339468227445729021, -3.268109542640674547, -1.786138375875142494E-14 ) ) ;
#17615=VERTEX_POINT ( 'NONE', #5234 ) ;
#17738=CARTESIAN_POINT ( 'NONE',  ( 4.000000000000003553, 1.935983797701078757, -0.2494693066162350648 ) ) ;
#17780=CARTESIAN_POINT ( 'NONE',  ( -4.000000000000000000, -2.309401076758531346, -0.3572655899081733644 ) ) ;
#17844=DIRECTION ( 'NONE',  ( -0.000000000000000000, -0.000000000000000000, 1.000000000000000000 ) ) ;
#17847=CONICAL_SURFACE ( 'NONE', #20539, 2.060000000000000941, 0.9599310885968777018 ) ;
#17860=DIRECTION ( 'NONE',  ( 1.000000000000000000, 0.000000000000000000, 0.000000000000000000 ) ) ;
#17876=CARTESIAN_POINT ( 'NONE',  ( -2.271448787322325728E-15, -4.618802153517061804, -5.599999999999999645 ) ) ;
#17885=B_SPLINE_CURVE_WITH_KNOTS ( 'NONE', 3,
 ( #2030, #6898, #4794, #19309, #17738, #3211 ),
 .UNSPECIFIED., .F., .F.,
 ( 4, 2, 4 ),
 ( 0.006456566858647416578, 0.007625406818786683791, 0.008794246778925951871 ),
 .UNSPECIFIED. ) ;
#17899=EDGE_CURVE ( 'NONE', #17615, #232, #1080, .T. ) ;
#17903=AXIS2_PLACEMENT_3D ( 'NONE', #10931, #19201, #4681 ) ;
#17905=CARTESIAN_POINT ( 'NONE',  ( -2.099999999999999645, 2.571758278209440971E-16, -5.294516984716111097 ) ) ;
#17925=CARTESIAN_POINT ( 'NONE',  ( 0.000000000000000000, 0.000000000000000000, 3.469446951953614189E-15 ) ) ;
#18005=ORIENTED_EDGE ( 'NONE', *, *, #5847, .T. ) ;
#18026=CIRCLE ( 'NONE', #4198, 2.099999999999999645 ) ;
#18028=CARTESIAN_POINT ( 'NONE',  ( 4.000000000000000000, 0.000000000000000000, 0.000000000000000000 ) ) ;
#18046=DIRECTION ( 'NONE',  ( 1.000000000000000000, 0.000000000000000000, 0.000000000000000000 ) ) ;
#18057=CARTESIAN_POINT ( 'NONE',  ( 0.000000000000000000, 0.000000000000000000, -0.3080913168122707546 ) ) ;
#18126=CARTESIAN_POINT ( 'NONE',  ( -2.000000000000009770, 3.464101615137749057, -5.600000000000000533 ) ) ;
#18153=CIRCLE ( 'NONE', #20856, 4.000000000000000000 ) ;
#18199=DIRECTION ( 'NONE',  ( -1.000000000000000000, 0.000000000000000000, 0.000000000000000000 ) ) ;
#18224=B_SPLINE_CURVE_WITH_KNOTS ( 'NONE', 3,
 ( #18460, #3715, #17085, #20139, #6904, #15177 ),
 .UNSPECIFIED., .F., .F.,
 ( 4, 2, 4 ),
 ( 0.006456566858647417445, 0.007625406818786684658, 0.008794246778925951871 ),
 .UNSPECIFIED. ) ;
#18299=EDGE_CURVE ( 'NONE', #13448, #12949, #4886, .T. ) ;
#18301=VECTOR ( 'NONE', #6052, 1000.000000000000114 ) ;
#18313=EDGE_LOOP ( 'NONE', ( #14080, #2773, #6408 ) ) ;
#18377=EDGE_CURVE ( 'NONE', #4533, #20501, #18224, .T. ) ;
#18406=B_SPLINE_CURVE_WITH_KNOTS ( 'NONE', 3,
 ( #13784, #4234, #2748, #2428, #6035, #18766 ),
 .UNSPECIFIED., .F., .F.,
 ( 4, 2, 4 ),
 ( 0.002336974151641521731, 0.003500975885716455828, 0.004664977619791389925 ),
 .UNSPECIFIED. ) ;
#18414=ADVANCED_FACE ( 'NONE', ( #13491 ), #12203, .T. ) ;
#18438=EDGE_CURVE ( 'NONE', #12005, #4533, #15591, .T. ) ;
#18439=CARTESIAN_POINT ( 'NONE',  ( -4.000000000000000000, 2.309401076758531346, -5.242734410091827613 ) ) ;
#18460=CARTESIAN_POINT ( 'NONE',  ( 4.000000000000000000, 0.000000000000000000, -5.600000000000000533 ) ) ;
#18476=ORIENTED_EDGE ( 'NONE', *, *, #7534, .F. ) ;
#18500=CONICAL_SURFACE ( 'NONE', #5671, 4.000000000000000000, 1.047197551196595855 ) ;
#18504=EDGE_CURVE ( 'NONE', #701, #12949, #7643, .T. ) ;
#18543=( LENGTH_UNIT ( ) NAMED_UNIT ( * ) SI_UNIT ( .MILLI., .METRE. ) );
#18568=CARTESIAN_POINT ( 'NONE',  ( 2.000000000000027089, 3.464101615137739731, 0.000000000000000000 ) ) ;
#18574=ADVANCED_FACE ( 'NONE', ( #12747 ), #12485, .T. ) ;
#18595=SURFACE_STYLE_USAGE ( .BOTH. , #12127 ) ;
#18601=CARTESIAN_POINT ( 'NONE',  ( -4.000000000000000000, -2.309401076758531346, -0.3572655899081733644 ) ) ;
#18623=CARTESIAN_POINT ( 'NONE',  ( -2.000000000000022649, -3.464101615137742396, -5.600000000000000533 ) ) ;
#18663=EDGE_CURVE ( 'NONE', #15454, #988, #16895, .T. ) ;
#18672=EDGE_LOOP ( 'NONE', ( #10968, #5262, #1260 ) ) ;
#18693=CARTESIAN_POINT ( 'NONE',  ( -4.000000000000000000, 1.935983797701083420, -5.350530693383767300 ) ) ;
#18710=CARTESIAN_POINT ( 'NONE',  ( 2.060000000000000941, 0.000000000000000000, -0.3080913168122707546 ) ) ;
#18754=( NAMED_UNIT ( * ) SI_UNIT ( $, .STERADIAN. ) SOLID_ANGLE_UNIT ( ) );
#18758=CARTESIAN_POINT ( 'NONE',  ( 2.339468227445713921, 3.268109542640642573, 2.447078184617672891E-15 ) ) ;
#18765=ADVANCED_FACE ( 'NONE', ( #20887 ), #5315, .T. ) ;
#18766=CARTESIAN_POINT ( 'NONE',  ( -7.632783294297951215E-14, -4.618802153517020948, -0.3572655899081733644 ) ) ;
#18798=ORIENTED_EDGE ( 'NONE', *, *, #6886, .T. ) ;
#18828=FACE_OUTER_BOUND ( 'NONE', #10038, .T. ) ;
#18865=CARTESIAN_POINT ( 'NONE',  ( 3.673643420401899728, 2.497823135841253706, -0.2484800633749943699 ) ) ;
#18886=CONICAL_SURFACE ( 'NONE', #15783, 4.000000000000000000, 1.047197551196595855 ) ;
#18918=ORIENTED_EDGE ( 'NONE', *, *, #4188, .F. ) ;
#18929=ORIENTED_EDGE ( 'NONE', *, *, #15226, .T. ) ;
#18933=CARTESIAN_POINT ( 'NONE',  ( 4.000000000000000000, 0.000000000000000000, -5.600000000000000533 ) ) ;
#18940=EDGE_CURVE ( 'NONE', #6927, #8003, #13165, .T. ) ;
#19032=CARTESIAN_POINT ( 'NONE',  ( 4.000000000000004441, -1.549102112939112486, -5.442104661404058241 ) ) ;
#19050=CARTESIAN_POINT ( 'NONE',  ( -7.459310946700270506E-14, -4.618802153517020948, -5.242734410091827613 ) ) ;
#19106=CARTESIAN_POINT ( 'NONE',  ( 2.500000000000000444, 0.000000000000000000, 3.469446951953614189E-15 ) ) ;
#19115=LINE ( 'NONE', #16030, #15829 ) ;
#19125=CARTESIAN_POINT ( 'NONE',  ( -1.321505333908964186, 3.855830693249140850, -0.03421028094653189716 ) ) ;
#19189=EDGE_LOOP ( 'NONE', ( #12707, #18005, #7601 ) ) ;
#19192=DIRECTION ( 'NONE',  ( 0.000000000000000000, 0.000000000000000000, 1.000000000000000000 ) ) ;
#19200=CARTESIAN_POINT ( 'NONE',  ( -2.500000000000002220, 0.000000000000000000, -5.574599999999999334 ) ) ;
#19201=DIRECTION ( 'NONE',  ( -0.000000000000000000, -0.000000000000000000, 1.000000000000000000 ) ) ;
#19220=CARTESIAN_POINT ( 'NONE',  ( 0.000000000000000000, 0.000000000000000000, -5.600000000000000533 ) ) ;
#19253=CARTESIAN_POINT ( 'NONE',  ( -4.000000000000000000, 0.000000000000000000, 0.000000000000000000 ) ) ;
#19261=EDGE_LOOP ( 'NONE', ( #6803, #465 ) ) ;
#19309=CARTESIAN_POINT ( 'NONE',  ( 4.000000000000003553, 1.557668341133516154, -0.1596965656957575475 ) ) ;
#19325=DIRECTION ( 'NONE',  ( -0.000000000000000000, -0.000000000000000000, 1.000000000000000000 ) ) ;
#19356=CARTESIAN_POINT ( 'NONE',  ( 0.000000000000000000, 0.000000000000000000, -25.03750572909317285 ) ) ;
#19362=AXIS2_PLACEMENT_3D ( 'NONE', #2223, #14846, #8682 ) ;
#19374=ORIENTED_EDGE ( 'NONE', *, *, #18438, .T. ) ;
#19381=ORIENTED_EDGE ( 'NONE', *, *, #17387, .T. ) ;
#19414=VERTEX_POINT ( 'NONE', #18601 ) ;
#19427=DIRECTION ( 'NONE',  ( -0.000000000000000000, -0.000000000000000000, 1.000000000000000000 ) ) ;
#19441=CONICAL_SURFACE ( 'NONE', #20800, 4.000000000000000000, 1.047197551196595855 ) ;
#19450=CARTESIAN_POINT ( 'NONE',  ( -7.632783294297951215E-14, -4.618802153517020948, -0.3572655899081733644 ) ) ;
#19474=CARTESIAN_POINT ( 'NONE',  ( 0.000000000000000000, 0.000000000000000000, 0.000000000000000000 ) ) ;
#19534=ORIENTED_EDGE ( 'NONE', *, *, #3794, .T. ) ;
#19570=FACE_OUTER_BOUND ( 'NONE', #157, .T. ) ;
#19575=B_SPLINE_CURVE_WITH_KNOTS ( 'NONE', 3,
 ( #19253, #6624, #7917, #6323, #4633, #11502 ),
 .UNSPECIFIED., .F., .F.,
 ( 4, 2, 4 ),
 ( 0.006456566858647395761, 0.007625406818786647362, 0.008794246778925899830 ),
 .UNSPECIFIED. ) ;
#19611=CARTESIAN_POINT ( 'NONE',  ( -3.345653888883671989, 2.687187980154694511, -0.1391502195351393412 ) ) ;
#19631=DIRECTION ( 'NONE',  ( -0.000000000000000000, -0.000000000000000000, 1.000000000000000000 ) ) ;
#19685=VERTEX_POINT ( 'NONE', #16254 ) ;
#19696=( LENGTH_UNIT ( ) NAMED_UNIT ( * ) SI_UNIT ( .MILLI., .METRE. ) );
#19718=EDGE_CURVE ( 'NONE', #4533, #1320, #16136, .T. ) ;
#19720=ORIENTED_EDGE ( 'NONE', *, *, #13401, .F. ) ;
#19735=CARTESIAN_POINT ( 'NONE',  ( 0.000000000000000000, 0.000000000000000000, -5.574599999999999334 ) ) ;
#19743=FACE_OUTER_BOUND ( 'NONE', #2885, .T. ) ;
#19753=CIRCLE ( 'NONE', #1167, 2.500000000000002220 ) ;
#19760=CARTESIAN_POINT ( 'NONE',  ( -2.000000000000022649, -3.464101615137742396, 0.000000000000000000 ) ) ;
#19777=CARTESIAN_POINT ( 'NONE',  ( 0.000000000000000000, 0.000000000000000000, 0.000000000000000000 ) ) ;
#19791=ORIENTED_EDGE ( 'NONE', *, *, #13261, .T. ) ;
#19868=AXIS2_PLACEMENT_3D ( 'NONE', #20452, #4443, #15785 ) ;
#19994=ORIENTED_EDGE ( 'NONE', *, *, #5685, .T. ) ;
#20042=DIRECTION ( 'NONE',  ( 0.000000000000000000, 0.000000000000000000, 1.000000000000000000 ) ) ;
#20073=CARTESIAN_POINT ( 'NONE',  ( -4.000000000000000000, -2.309401076758525573, -5.599999999999999645 ) ) ;
#20093=CARTESIAN_POINT ( 'NONE',  ( -2.000000000000022649, -3.464101615137742396, 0.000000000000000000 ) ) ;
#20109=CARTESIAN_POINT ( 'NONE',  ( 0.000000000000000000, 0.000000000000000000, -0.3080913168122707546 ) ) ;
#20123=CARTESIAN_POINT ( 'NONE',  ( 2.000000000000027089, 3.464101615137739731, -5.600000000000000533 ) ) ;
#20139=CARTESIAN_POINT ( 'NONE',  ( 4.000000000000002665, 1.557668341133517043, -5.440303434304241570 ) ) ;
#20157=DIRECTION ( 'NONE',  ( -1.000000000000000000, 0.000000000000000000, 0.000000000000000000 ) ) ;
#20168=SURFACE_STYLE_FILL_AREA ( #7236 ) ;
#20199=EDGE_CURVE ( 'NONE', #5038, #19685, #19575, .T. ) ;
#20203=FACE_OUTER_BOUND ( 'NONE', #1948, .T. ) ;
#20237=EDGE_CURVE ( 'NONE', #232, #19414, #97, .T. ) ;
#20245=VERTEX_POINT ( 'NONE', #13109 ) ;
#20288=CARTESIAN_POINT ( 'NONE',  ( 0.000000000000000000, 0.000000000000000000, -5.600000000000000533 ) ) ;
#20294=CARTESIAN_POINT ( 'NONE',  ( -4.000000000000000000, 0.000000000000000000, -5.599999999999999645 ) ) ;
#20302=ORIENTED_EDGE ( 'NONE', *, *, #13067, .T. ) ;
#20327=ORIENTED_EDGE ( 'NONE', *, *, #20199, .T. ) ;
#20333=CARTESIAN_POINT ( 'NONE',  ( 0.000000000000000000, 0.000000000000000000, -5.599999999999999645 ) ) ;
#20423=B_SPLINE_CURVE_WITH_KNOTS ( 'NONE', 3,
 ( #5319, #11787, #3716, #2368, #10322, #8729 ),
 .UNSPECIFIED., .F., .F.,
 ( 4, 2, 4 ),
 ( 0.004120275011746842714, 0.005288420935197119671, 0.006456566858647395761 ),
 .UNSPECIFIED. ) ;
#20452=CARTESIAN_POINT ( 'NONE',  ( 0.000000000000000000, 0.000000000000000000, -0.2800830152838832965 ) ) ;
#20454=CARTESIAN_POINT ( 'NONE',  ( 0.000000000000000000, 0.000000000000000000, -5.599999999999999645 ) ) ;
#20480=DIRECTION ( 'NONE',  ( 0.000000000000000000, 0.000000000000000000, 1.000000000000000000 ) ) ;
#20490=EDGE_CURVE ( 'NONE', #6927, #19685, #19115, .T. ) ;
#20493=CARTESIAN_POINT ( 'NONE',  ( -1.660531772554312280, 3.660093687634848436, 2.744386749103932310E-15 ) ) ;
#20500=MECHANICAL_DESIGN_GEOMETRIC_PRESENTATION_REPRESENTATION('',(#16758),#11370);
#20501=VERTEX_POINT ( 'NONE', #15819 ) ;
#20508=CARTESIAN_POINT ( 'NONE',  ( 4.000000000000003553, 2.309401076758524685, -0.3572655899081733644 ) ) ;
#20539=AXIS2_PLACEMENT_3D ( 'NONE', #20109, #628, #13769 ) ;
#20597=CARTESIAN_POINT ( 'NONE',  ( -0.3263565795980851170, 4.430380094434251959, -0.2484800633750073040 ) ) ;
#20632=DIRECTION ( 'NONE',  ( 1.000000000000000000, 0.000000000000000000, 0.000000000000000000 ) ) ;
#20643=CARTESIAN_POINT ( 'NONE',  ( 2.000000000000027089, 3.464101615137739731, 0.000000000000000000 ) ) ;
#20707=ORIENTED_EDGE ( 'NONE', *, *, #13067, .F. ) ;
#20720=EDGE_LOOP ( 'NONE', ( #13135, #9675, #9799, #4423, #3570, #9 ) ) ;
#20723=CARTESIAN_POINT ( 'NONE',  ( 0.000000000000000000, 0.000000000000000000, -5.599999999999999645 ) ) ;
#20747=FACE_OUTER_BOUND ( 'NONE', #5228, .T. ) ;
#20748=CIRCLE ( 'NONE', #11289, 2.099999999999999645 ) ;
#20759=DIRECTION ( 'NONE',  ( -0.8660254037844348218, 0.5000000000000066613, 0.000000000000000000 ) ) ;
#20780=LINE ( 'NONE', #19200, #10200 ) ;
#20800=AXIS2_PLACEMENT_3D ( 'NONE', #1204, #4687, #12430 ) ;
#20811=ADVANCED_FACE ( 'NONE', ( #20747 ), #7937, .T. ) ;
#20830=ORIENTED_EDGE ( 'NONE', *, *, #10670, .F. ) ;
#20856=AXIS2_PLACEMENT_3D ( 'NONE', #8521, #6936, #10126 ) ;
#20858=CARTESIAN_POINT ( 'NONE',  ( 4.000000000000003553, -2.309401076758539784, -5.599999999999999645 ) ) ;
#20866=CIRCLE ( 'NONE', #11732, 4.000000000000000888 ) ;
#20887=FACE_OUTER_BOUND ( 'NONE', #16373, .T. ) ;
#20896=ORIENTED_EDGE ( 'NONE', *, *, #15226, .F. ) ;
#20918=CARTESIAN_POINT ( 'NONE',  ( 1.084202172485504434E-14, 4.618802153517020059, -5.242734410091827613 ) ) ;
#20922=DIRECTION ( 'NONE',  ( 0.000000000000000000, 0.000000000000000000, -1.000000000000000000 ) ) ;
ENDSEC;
END-ISO-10303-21;
